ISO-10303-21;
HEADER;
/* Generated by software containing ST-Developer
 * from STEP Tools, Inc. (www.steptools.com) 
 */

FILE_DESCRIPTION(
/* description */ ('STEP AP214'),
/* implementation_level */ '2;1');

FILE_NAME(
/* name */ 'Hex Nut M5.step',
/* time_stamp */ '2026-11-14T06:10:26-08:00',
/* author */ (''),
/* organization */ (''),
/* preprocessor_version */ 'ST-DEVELOPER v20.2',
/* originating_system */ 'Autodesk Translation Framework v15.17.0.0',
/* authorisation */ '');

FILE_SCHEMA (('AUTOMOTIVE_DESIGN { 1 0 10303 214 3 1 1 }'));
ENDSEC;

DATA;
#10=MECHANICAL_DESIGN_GEOMETRIC_PRESENTATION_REPRESENTATION('',(#171),#10413);
#75=(
BOUNDED_SURFACE()
B_SPLINE_SURFACE(1,2,((#10054,#10055,#10056,#10057,#10058,#10059,#10060,
#10061,#10062,#10063,#10064,#10065,#10066,#10067,#10068,#10069,#10070,#10071,
#10072,#10073,#10074,#10075,#10076,#10077,#10078,#10079,#10080,#10081,#10082,
#10083,#10084,#10085,#10086,#10087,#10088,#10089,#10090,#10091,#10092,#10093,
#10094,#10095,#10096,#10097,#10098,#10099,#10100,#10101,#10102,#10103,#10104,
#10105,#10106,#10107,#10108,#10109,#10110,#10111,#10112,#10113,#10114,#10115,
#10116,#10117,#10118,#10119,#10120,#10121,#10122,#10123,#10124,#10125,#10126,
#10127,#10128,#10129,#10130,#10131,#10132,#10133,#10134),(#10135,#10136,
#10137,#10138,#10139,#10140,#10141,#10142,#10143,#10144,#10145,#10146,#10147,
#10148,#10149,#10150,#10151,#10152,#10153,#10154,#10155,#10156,#10157,#10158,
#10159,#10160,#10161,#10162,#10163,#10164,#10165,#10166,#10167,#10168,#10169,
#10170,#10171,#10172,#10173,#10174,#10175,#10176,#10177,#10178,#10179,#10180,
#10181,#10182,#10183,#10184,#10185,#10186,#10187,#10188,#10189,#10190,#10191,
#10192,#10193,#10194,#10195,#10196,#10197,#10198,#10199,#10200,#10201,#10202,
#10203,#10204,#10205,#10206,#10207,#10208,#10209,#10210,#10211,#10212,#10213,
#10214,#10215)),.UNSPECIFIED.,.F.,.F.,.F.)
B_SPLINE_SURFACE_WITH_KNOTS((2,2),(3,2,2,2,2,2,2,2,2,2,2,2,2,2,2,2,2,2,
2,2,2,2,2,2,2,2,2,2,2,2,2,2,2,2,2,2,2,2,2,2,3),(-8.46272100971598E-5,1.),
(0.,0.025,0.05,0.075,0.1,0.125,0.15,0.175,0.2,0.225,0.25,0.275,0.3,0.325,
0.35,0.375,0.4,0.425,0.45,0.475,0.5,0.525,0.55,0.575,0.6,0.625,0.65,0.675,
0.7,0.725,0.75,0.775,0.8,0.825,0.85,0.875,0.9,0.925,0.95,0.975,1.),
 .UNSPECIFIED.)
GEOMETRIC_REPRESENTATION_ITEM()
RATIONAL_B_SPLINE_SURFACE(((1.,0.923879532511287,1.,0.923879532511287,1.,
0.923879532511287,1.,0.923879532511287,1.,0.923879532511287,1.,0.923879532511287,
1.,0.923879532511287,1.,0.923879532511287,1.,0.923879532511287,1.,0.923879532511287,
1.,0.923879532511287,1.,0.923879532511287,1.,0.923879532511287,1.,0.923879532511287,
1.,0.923879532511287,1.,0.923879532511287,1.,0.923879532511287,1.,0.923879532511287,
1.,0.923879532511287,1.,0.923879532511287,1.,0.923879532511287,1.,0.923879532511287,
1.,0.923879532511287,1.,0.923879532511287,1.,0.923879532511287,1.,0.923879532511287,
1.,0.923879532511287,1.,0.923879532511287,1.,0.923879532511287,1.,0.923879532511287,
1.,0.923879532511287,1.,0.923879532511287,1.,0.923879532511287,1.,0.923879532511287,
1.,0.923879532511287,1.,0.923879532511287,1.,0.923879532511287,1.,0.923879532511287,
1.,0.923879532511287,1.,0.923879532511287,1.),(1.,0.923879532511287,1.,
0.923879532511287,1.,0.923879532511287,1.,0.923879532511287,1.,0.923879532511287,
1.,0.923879532511287,1.,0.923879532511287,1.,0.923879532511287,1.,0.923879532511287,
1.,0.923879532511287,1.,0.923879532511287,1.,0.923879532511287,1.,0.923879532511287,
1.,0.923879532511287,1.,0.923879532511287,1.,0.923879532511287,1.,0.923879532511287,
1.,0.923879532511287,1.,0.923879532511287,1.,0.923879532511287,1.,0.923879532511287,
1.,0.923879532511287,1.,0.923879532511287,1.,0.923879532511287,1.,0.923879532511287,
1.,0.923879532511287,1.,0.923879532511287,1.,0.923879532511287,1.,0.923879532511287,
1.,0.923879532511287,1.,0.923879532511287,1.,0.923879532511287,1.,0.923879532511287,
1.,0.923879532511287,1.,0.923879532511287,1.,0.923879532511287,1.,0.923879532511287,
1.,0.923879532511287,1.,0.923879532511287,1.,0.923879532511287,1.)))
REPRESENTATION_ITEM('')
SURFACE()
);
#76=(
BOUNDED_SURFACE()
B_SPLINE_SURFACE(1,2,((#10216,#10217,#10218,#10219,#10220,#10221,#10222,
#10223,#10224,#10225,#10226,#10227,#10228,#10229,#10230,#10231,#10232,#10233,
#10234,#10235,#10236,#10237,#10238,#10239,#10240,#10241,#10242,#10243,#10244,
#10245,#10246,#10247,#10248,#10249,#10250,#10251,#10252,#10253,#10254,#10255,
#10256,#10257,#10258,#10259,#10260,#10261,#10262,#10263,#10264,#10265,#10266,
#10267,#10268,#10269,#10270,#10271,#10272,#10273,#10274,#10275,#10276,#10277,
#10278,#10279,#10280,#10281,#10282,#10283,#10284,#10285,#10286,#10287,#10288,
#10289,#10290,#10291,#10292,#10293,#10294,#10295,#10296),(#10297,#10298,
#10299,#10300,#10301,#10302,#10303,#10304,#10305,#10306,#10307,#10308,#10309,
#10310,#10311,#10312,#10313,#10314,#10315,#10316,#10317,#10318,#10319,#10320,
#10321,#10322,#10323,#10324,#10325,#10326,#10327,#10328,#10329,#10330,#10331,
#10332,#10333,#10334,#10335,#10336,#10337,#10338,#10339,#10340,#10341,#10342,
#10343,#10344,#10345,#10346,#10347,#10348,#10349,#10350,#10351,#10352,#10353,
#10354,#10355,#10356,#10357,#10358,#10359,#10360,#10361,#10362,#10363,#10364,
#10365,#10366,#10367,#10368,#10369,#10370,#10371,#10372,#10373,#10374,#10375,
#10376,#10377)),.UNSPECIFIED.,.F.,.F.,.F.)
B_SPLINE_SURFACE_WITH_KNOTS((2,2),(3,2,2,2,2,2,2,2,2,2,2,2,2,2,2,2,2,2,
2,2,2,2,2,2,2,2,2,2,2,2,2,2,2,2,2,2,2,2,2,2,3),(0.,1.00002043531825),(0.,
0.025,0.05,0.075,0.1,0.125,0.15,0.175,0.2,0.225,0.25,0.275,0.3,0.325,0.35,
0.375,0.4,0.425,0.45,0.475,0.5,0.525,0.55,0.575,0.6,0.625,0.65,0.675,0.7,
0.725,0.75,0.775,0.8,0.825,0.85,0.875,0.9,0.925,0.95,0.975,1.),
 .UNSPECIFIED.)
GEOMETRIC_REPRESENTATION_ITEM()
RATIONAL_B_SPLINE_SURFACE(((1.,0.923879532511287,1.,0.923879532511287,1.,
0.923879532511287,1.,0.923879532511287,1.,0.923879532511287,1.,0.923879532511287,
1.,0.923879532511287,1.,0.923879532511287,1.,0.923879532511287,1.,0.923879532511287,
1.,0.923879532511287,1.,0.923879532511287,1.,0.923879532511287,1.,0.923879532511287,
1.,0.923879532511287,1.,0.923879532511287,1.,0.923879532511287,1.,0.923879532511287,
1.,0.923879532511287,1.,0.923879532511287,1.,0.923879532511287,1.,0.923879532511287,
1.,0.923879532511287,1.,0.923879532511287,1.,0.923879532511287,1.,0.923879532511287,
1.,0.923879532511287,1.,0.923879532511287,1.,0.923879532511287,1.,0.923879532511287,
1.,0.923879532511287,1.,0.923879532511287,1.,0.923879532511287,1.,0.923879532511287,
1.,0.923879532511287,1.,0.923879532511287,1.,0.923879532511287,1.,0.923879532511287,
1.,0.923879532511287,1.,0.923879532511287,1.),(1.,0.923879532511287,1.,
0.923879532511287,1.,0.923879532511287,1.,0.923879532511287,1.,0.923879532511287,
1.,0.923879532511287,1.,0.923879532511287,1.,0.923879532511287,1.,0.923879532511287,
1.,0.923879532511287,1.,0.923879532511287,1.,0.923879532511287,1.,0.923879532511287,
1.,0.923879532511287,1.,0.923879532511287,1.,0.923879532511287,1.,0.923879532511287,
1.,0.923879532511287,1.,0.923879532511287,1.,0.923879532511287,1.,0.923879532511287,
1.,0.923879532511287,1.,0.923879532511287,1.,0.923879532511287,1.,0.923879532511287,
1.,0.923879532511287,1.,0.923879532511287,1.,0.923879532511287,1.,0.923879532511287,
1.,0.923879532511287,1.,0.923879532511287,1.,0.923879532511287,1.,0.923879532511287,
1.,0.923879532511287,1.,0.923879532511287,1.,0.923879532511287,1.,0.923879532511287,
1.,0.923879532511287,1.,0.923879532511287,1.,0.923879532511287,1.)))
REPRESENTATION_ITEM('')
SURFACE()
);
#77=B_SPLINE_CURVE_WITH_KNOTS('',3,(#9606,#9607,#9608,#9609,#9610,#9611,
#9612,#9613,#9614,#9615,#9616,#9617),.UNSPECIFIED.,.F.,.F.,(4,2,2,2,2,4),
(0.,0.0440198106719265,0.0818393800786219,0.0973901488912384,0.118004089223957,
0.138865194736436),.UNSPECIFIED.);
#78=B_SPLINE_CURVE_WITH_KNOTS('',3,(#9624,#9625,#9626,#9627,#9628,#9629,
#9630,#9631,#9632,#9633,#9634,#9635,#9636,#9637),.UNSPECIFIED.,.F.,.F.,
(4,2,2,2,2,2,4),(0.65296058419034,0.667191402073545,0.721861714124772,0.750052142288269,
0.80044940087167,0.822940957368803,0.845554952657274),.UNSPECIFIED.);
#79=B_SPLINE_CURVE_WITH_KNOTS('',3,(#9641,#9642,#9643,#9644,#9645,#9646,
#9647,#9648,#9649,#9650),.UNSPECIFIED.,.F.,.F.,(4,2,2,2,4),(0.,0.0725503805935694,
0.183171338078937,0.39459654609614,0.611301898072818),.UNSPECIFIED.);
#80=B_SPLINE_CURVE_WITH_KNOTS('',3,(#9656,#9657,#9658,#9659,#9660,#9661,
#9662,#9663,#9664,#9665,#9666,#9667,#9668,#9669,#9670,#9671,#9672,#9673,
#9674,#9675,#9676,#9677,#9678,#9679,#9680,#9681,#9682,#9683),
 .UNSPECIFIED.,.F.,.F.,(4,2,2,2,2,2,2,2,2,2,2,2,2,4),(2.8604222096497,2.92399815097309,
3.00151852083596,3.07984339341042,3.15735934738356,3.23558227378115,3.31309753786526,
3.39121939156188,3.46873767665382,3.54675946426518,3.62428444893176,3.70220732091536,
3.75130237269173,3.79952779459516),.UNSPECIFIED.);
#81=B_SPLINE_CURVE_WITH_KNOTS('',3,(#9684,#9685,#9686,#9687,#9688,#9689,
#9690,#9691,#9692,#9693,#9694,#9695,#9696,#9697,#9698,#9699,#9700,#9701,
#9702,#9703,#9704,#9705,#9706,#9707,#9708,#9709,#9710,#9711,#9712,#9713,
#9714,#9715,#9716,#9717,#9718,#9719),.UNSPECIFIED.,.F.,.F.,(4,2,2,2,2,2,
2,2,2,2,2,2,2,2,2,2,2,4),(9.99999999976564E-7,0.0723571430117073,0.145111301826658,
0.22257528520235,0.302853983952927,0.38026926760894,0.460477482838669,0.537847198345145,
0.617986080669744,0.695313511929628,0.775384190116896,0.852672774273399,
0.932676349504524,1.00992967673158,1.08986721715565,1.16708902919314,1.24696156497064,
1.26600100077784),.UNSPECIFIED.);
#82=B_SPLINE_CURVE_WITH_KNOTS('',3,(#9724,#9725,#9726,#9727,#9728,#9729,
#9730,#9731,#9732,#9733,#9734,#9735,#9736,#9737,#9738,#9739,#9740,#9741,
#9742,#9743,#9744,#9745,#9746,#9747,#9748,#9749,#9750,#9751,#9752,#9753,
#9754,#9755,#9756,#9757,#9758,#9759),.UNSPECIFIED.,.F.,.F.,(4,2,2,2,2,2,
2,2,2,2,2,2,2,2,2,2,2,4),(1.60361927798793,1.67068837178043,1.75059716351924,
1.82756418592221,1.90739668701968,1.98645074137197,2.06407483714533,2.14302368536841,
2.22062153982352,2.29946541005855,2.37704053193709,2.45577971634894,2.53333568134052,
2.61197054470874,2.68951098486698,2.76804197371372,2.84557056555073,2.8604222096497),
 .UNSPECIFIED.);
#83=B_SPLINE_CURVE_WITH_KNOTS('',3,(#9760,#9761,#9762,#9763,#9764,#9765,
#9766,#9767,#9768,#9769,#9770,#9771,#9772,#9773,#9774,#9775,#9776,#9777,
#9778,#9779,#9780,#9781,#9782,#9783,#9784,#9785,#9786,#9787,#9788,#9789,
#9790,#9791,#9792,#9793,#9794,#9795),.UNSPECIFIED.,.F.,.F.,(4,2,2,2,2,2,
2,2,2,2,2,2,2,2,2,2,2,4),(1.26600100077784,1.32415579820781,1.40396438029636,
1.48113503862289,1.56088054628166,1.63803178784153,1.71771511568453,1.79485124435928,
1.87447323848536,1.95159867942297,2.03003619734553,2.1081949238022,2.18666282399953,
2.26473464872532,2.34323576121314,2.42122333365511,2.49976031435316,2.52861029293173),
 .UNSPECIFIED.);
#84=B_SPLINE_CURVE_WITH_KNOTS('',3,(#9800,#9801,#9802,#9803),
 .UNSPECIFIED.,.F.,.F.,(4,4),(3.78986857128077,3.8120765287242),
 .UNSPECIFIED.);
#85=B_SPLINE_CURVE_WITH_KNOTS('',3,(#9804,#9805,#9806,#9807,#9808,#9809,
#9810,#9811,#9812,#9813,#9814,#9815,#9816,#9817),.UNSPECIFIED.,.F.,.F.,
(4,2,2,2,2,2,4),(9.99999999715276E-7,0.046357433654922,0.0937119022879353,
0.174442583515723,0.25212318836089,0.332767216413102,0.339556120788476),
 .UNSPECIFIED.);
#86=B_SPLINE_CURVE_WITH_KNOTS('',3,(#9819,#9820,#9821,#9822,#9823,#9824,
#9825,#9826,#9827,#9828,#9829,#9830,#9831,#9832,#9833,#9834,#9835,#9836,
#9837,#9838,#9839,#9840,#9841,#9842,#9843,#9844,#9845,#9846,#9847,#9848,
#9849,#9850,#9851,#9852,#9853,#9854),.UNSPECIFIED.,.F.,.F.,(4,2,2,2,2,2,
2,2,2,2,2,2,2,2,2,2,2,4),(0.339556120788476,0.41036939162952,0.490927908821085,
0.568452828064013,0.648926534411366,0.726375625006592,0.806765489869361,
0.884140289007795,0.964447312664774,1.04174945254203,1.12197466490902,1.1992058779733,
1.27935033693266,1.35651246121441,1.43657725052838,1.5136722350114,1.5936584617954,
1.60361927798793),.UNSPECIFIED.);
#87=B_SPLINE_CURVE_WITH_KNOTS('',3,(#9855,#9856,#9857,#9858,#9859,#9860,
#9861,#9862,#9863,#9864,#9865,#9866,#9867,#9868,#9869,#9870,#9871,#9872,
#9873,#9874,#9875,#9876,#9877,#9878,#9879,#9880,#9881,#9882,#9883,#9884,
#9885,#9886,#9887,#9888,#9889,#9890),.UNSPECIFIED.,.F.,.F.,(4,2,2,2,2,2,
2,2,2,2,2,2,2,2,2,2,2,4),(2.52861029293173,2.57766649346594,2.65624181672742,
2.73406967065805,2.8126856246171,2.89043842827534,2.9690971131827,3.0467783436143,
3.12548167324701,3.20309500277339,3.28184470891144,3.359393996049,3.43819163591573,
3.51568091413997,3.5945278806067,3.67196134507875,3.74273037840176,3.78986857128077),
 .UNSPECIFIED.);
#88=B_SPLINE_CURVE_WITH_KNOTS('',3,(#9926,#9927,#9928,#9929,#9930,#9931,
#9932,#9933,#9934,#9935,#9936,#9937,#9938,#9939,#9940,#9941,#9942,#9943,
#9944,#9945,#9946,#9947,#9948,#9949,#9950,#9951),.UNSPECIFIED.,.F.,.F.,
(4,2,2,2,2,2,2,2,2,2,2,2,4),(1.00000005114759E-6,0.0504044288517504,0.101697907474949,
0.196791682582806,0.281186634272934,0.358208836397077,0.426888278521547,
0.487555064818087,0.518648689337668,0.549949053437167,0.607608841009272,
0.637237664676633,0.65296058419034),.UNSPECIFIED.);
#89=B_SPLINE_CURVE_WITH_KNOTS('',3,(#9955,#9956,#9957,#9958,#9959,#9960,
#9961,#9962,#9963,#9964,#9965,#9966,#9967,#9968,#9969,#9970,#9971,#9972,
#9973,#9974,#9975,#9976,#9977,#9978,#9979,#9980,#9981,#9982,#9983,#9984,
#9985,#9986,#9987,#9988),.UNSPECIFIED.,.F.,.F.,(4,2,2,2,2,2,2,2,2,2,2,2,
2,2,2,2,4),(-0.463997948906847,-0.451682823252161,-0.441542190454548,-0.42099125853003,
-0.408322861738078,-0.395698404917208,-0.371037580166826,-0.34212985279081,
-0.311147419702825,-0.294752355985258,-0.261382300325676,-0.244928786327198,
-0.207389215554967,-0.164348973242395,-0.11566569854488,-0.0657340977400675,
-9.99999999292063E-7),.UNSPECIFIED.);
#114=(
BOUNDED_CURVE()
B_SPLINE_CURVE(2,(#9474,#9475,#9476,#9477,#9478,#9479,#9480,#9481,#9482,
#9483,#9484),.UNSPECIFIED.,.F.,.F.)
B_SPLINE_CURVE_WITH_KNOTS((3,2,2,2,2,3),(0.7,0.725,0.75,0.775,0.8,0.814142575738201),
 .UNSPECIFIED.)
CURVE()
GEOMETRIC_REPRESENTATION_ITEM()
RATIONAL_B_SPLINE_CURVE((1.,0.923879532511287,1.,0.923879532511287,1.,0.923879532511287,
1.,0.923879532511287,1.,0.956938420932543,0.962596973334531))
REPRESENTATION_ITEM('')
);
#115=(
BOUNDED_CURVE()
B_SPLINE_CURVE(2,(#9487,#9488,#9489,#9490,#9491,#9492,#9493,#9494,#9495,
#9496,#9497,#9498,#9499),.UNSPECIFIED.,.F.,.F.)
B_SPLINE_CURVE_WITH_KNOTS((3,2,2,2,2,2,3),(0.7,0.725,0.75,0.775,0.8,0.825,
0.839142575738204),.UNSPECIFIED.)
CURVE()
GEOMETRIC_REPRESENTATION_ITEM()
RATIONAL_B_SPLINE_CURVE((1.,0.923879532511287,1.,0.923879532511287,1.,0.923879532511287,
1.,0.923879532511287,1.,0.923879532511287,1.,0.956938420932534,0.962596973334533))
REPRESENTATION_ITEM('')
);
#116=(
BOUNDED_CURVE()
B_SPLINE_CURVE(2,(#9504,#9505,#9506,#9507,#9508,#9509,#9510,#9511,#9512,
#9513,#9514,#9515,#9516,#9517,#9518,#9519,#9520),.UNSPECIFIED.,.F.,.F.)
B_SPLINE_CURVE_WITH_KNOTS((3,2,2,2,2,2,2,2,3),(0.5,0.525,0.55,0.575,0.6,
0.625,0.65,0.675,0.7),.UNSPECIFIED.)
CURVE()
GEOMETRIC_REPRESENTATION_ITEM()
RATIONAL_B_SPLINE_CURVE((1.,0.923879532511287,1.,0.923879532511287,1.,0.923879532511287,
1.,0.923879532511287,1.,0.923879532511287,1.,0.923879532511287,1.,0.923879532511287,
1.,0.923879532511287,1.))
REPRESENTATION_ITEM('')
);
#117=(
BOUNDED_CURVE()
B_SPLINE_CURVE(2,(#9521,#9522,#9523,#9524,#9525,#9526,#9527,#9528,#9529,
#9530,#9531,#9532,#9533,#9534,#9535,#9536,#9537),.UNSPECIFIED.,.F.,.F.)
B_SPLINE_CURVE_WITH_KNOTS((3,2,2,2,2,2,2,2,3),(0.5,0.525,0.55,0.575,0.6,
0.625,0.65,0.675,0.7),.UNSPECIFIED.)
CURVE()
GEOMETRIC_REPRESENTATION_ITEM()
RATIONAL_B_SPLINE_CURVE((1.,0.923879532511287,1.,0.923879532511287,1.,0.923879532511287,
1.,0.923879532511287,1.,0.923879532511287,1.,0.923879532511287,1.,0.923879532511287,
1.,0.923879532511287,1.))
REPRESENTATION_ITEM('')
);
#118=(
BOUNDED_CURVE()
B_SPLINE_CURVE(2,(#9542,#9543,#9544,#9545,#9546,#9547,#9548,#9549,#9550,
#9551,#9552,#9553,#9554,#9555,#9556,#9557,#9558),.UNSPECIFIED.,.F.,.F.)
B_SPLINE_CURVE_WITH_KNOTS((3,2,2,2,2,2,2,2,3),(0.3,0.325,0.35,0.375,0.4,
0.425,0.45,0.475,0.5),.UNSPECIFIED.)
CURVE()
GEOMETRIC_REPRESENTATION_ITEM()
RATIONAL_B_SPLINE_CURVE((1.,0.923879532511287,1.,0.923879532511287,1.,0.923879532511287,
1.,0.923879532511287,1.,0.923879532511287,1.,0.923879532511287,1.,0.923879532511287,
1.,0.923879532511287,1.))
REPRESENTATION_ITEM('')
);
#119=(
BOUNDED_CURVE()
B_SPLINE_CURVE(2,(#9559,#9560,#9561,#9562,#9563,#9564,#9565,#9566,#9567,
#9568,#9569,#9570,#9571,#9572,#9573,#9574,#9575),.UNSPECIFIED.,.F.,.F.)
B_SPLINE_CURVE_WITH_KNOTS((3,2,2,2,2,2,2,2,3),(0.3,0.325,0.35,0.375,0.4,
0.425,0.45,0.475,0.5),.UNSPECIFIED.)
CURVE()
GEOMETRIC_REPRESENTATION_ITEM()
RATIONAL_B_SPLINE_CURVE((1.,0.923879532511287,1.,0.923879532511287,1.,0.923879532511287,
1.,0.923879532511287,1.,0.923879532511287,1.,0.923879532511287,1.,0.923879532511287,
1.,0.923879532511287,1.))
REPRESENTATION_ITEM('')
);
#120=(
BOUNDED_CURVE()
B_SPLINE_CURVE(2,(#9581,#9582,#9583,#9584,#9585,#9586,#9587),
 .UNSPECIFIED.,.F.,.F.)
B_SPLINE_CURVE_WITH_KNOTS((3,2,2,3),(0.0391425757382012,0.05,0.075,0.1),
 .UNSPECIFIED.)
CURVE()
GEOMETRIC_REPRESENTATION_ITEM()
RATIONAL_B_SPLINE_CURVE((0.962596973334531,0.966941111578743,1.,0.923879532511287,
1.,0.923879532511287,1.))
REPRESENTATION_ITEM('')
);
#121=(
BOUNDED_CURVE()
B_SPLINE_CURVE(2,(#9590,#9591,#9592,#9593,#9594,#9595,#9596,#9597,#9598),
 .UNSPECIFIED.,.F.,.F.)
B_SPLINE_CURVE_WITH_KNOTS((3,2,2,2,3),(0.0141425757382014,0.025,0.05,0.075,
0.1),.UNSPECIFIED.)
CURVE()
GEOMETRIC_REPRESENTATION_ITEM()
RATIONAL_B_SPLINE_CURVE((0.962596973334531,0.966941111578744,1.,0.923879532511287,
1.,0.923879532511287,1.,0.923879532511287,1.))
REPRESENTATION_ITEM('')
);
#122=(
BOUNDED_CURVE()
B_SPLINE_CURVE(2,(#9894,#9895,#9896),.UNSPECIFIED.,.F.,.F.)
B_SPLINE_CURVE_WITH_KNOTS((3,3),(-1.66699778258505,-0.74828608399493),
 .UNSPECIFIED.)
CURVE()
GEOMETRIC_REPRESENTATION_ITEM()
RATIONAL_B_SPLINE_CURVE((1.84251288693848,2.12755062252262,1.84251288693848))
REPRESENTATION_ITEM('')
);
#123=(
BOUNDED_CURVE()
B_SPLINE_CURVE(2,(#9898,#9899,#9900),.UNSPECIFIED.,.F.,.F.)
B_SPLINE_CURVE_WITH_KNOTS((3,3),(-1.66699778258506,-0.748286083994931),
 .UNSPECIFIED.)
CURVE()
GEOMETRIC_REPRESENTATION_ITEM()
RATIONAL_B_SPLINE_CURVE((1.84251288693848,2.12755062252262,1.84251288693848))
REPRESENTATION_ITEM('')
);
#124=(
BOUNDED_CURVE()
B_SPLINE_CURVE(2,(#9902,#9903,#9904),.UNSPECIFIED.,.F.,.F.)
B_SPLINE_CURVE_WITH_KNOTS((3,3),(-1.66699778258505,-0.748286083994929),
 .UNSPECIFIED.)
CURVE()
GEOMETRIC_REPRESENTATION_ITEM()
RATIONAL_B_SPLINE_CURVE((1.84251288693848,2.12755062252262,1.84251288693848))
REPRESENTATION_ITEM('')
);
#125=(
BOUNDED_CURVE()
B_SPLINE_CURVE(2,(#9906,#9907,#9908),.UNSPECIFIED.,.F.,.F.)
B_SPLINE_CURVE_WITH_KNOTS((3,3),(0.74828608399493,1.20764193328999),
 .UNSPECIFIED.)
CURVE()
GEOMETRIC_REPRESENTATION_ITEM()
RATIONAL_B_SPLINE_CURVE((1.84251288693848,1.98503175473055,1.98503175473055))
REPRESENTATION_ITEM('')
);
#126=(
BOUNDED_CURVE()
B_SPLINE_CURVE(2,(#9913,#9914,#9915),.UNSPECIFIED.,.F.,.F.)
B_SPLINE_CURVE_WITH_KNOTS((3,3),(1.20764193328999,1.66699778258505),
 .UNSPECIFIED.)
CURVE()
GEOMETRIC_REPRESENTATION_ITEM()
RATIONAL_B_SPLINE_CURVE((1.98503175473055,1.98503175473055,1.84251288693848))
REPRESENTATION_ITEM('')
);
#127=(
BOUNDED_CURVE()
B_SPLINE_CURVE(2,(#9917,#9918,#9919),.UNSPECIFIED.,.F.,.F.)
B_SPLINE_CURVE_WITH_KNOTS((3,3),(-1.66699778258506,-0.748286083994931),
 .UNSPECIFIED.)
CURVE()
GEOMETRIC_REPRESENTATION_ITEM()
RATIONAL_B_SPLINE_CURVE((1.84251288693848,2.12755062252262,1.84251288693848))
REPRESENTATION_ITEM('')
);
#128=(
BOUNDED_CURVE()
B_SPLINE_CURVE(2,(#9920,#9921,#9922),.UNSPECIFIED.,.F.,.F.)
B_SPLINE_CURVE_WITH_KNOTS((3,3),(-1.66699778258505,-0.748286083994929),
 .UNSPECIFIED.)
CURVE()
GEOMETRIC_REPRESENTATION_ITEM()
RATIONAL_B_SPLINE_CURVE((1.84251288693848,2.12755062252262,1.84251288693848))
REPRESENTATION_ITEM('')
);
#129=(
BOUNDED_CURVE()
B_SPLINE_CURVE(2,(#10020,#10021,#10022,#10023,#10024,#10025,#10026,#10027,
#10028,#10029,#10030,#10031,#10032,#10033,#10034,#10035,#10036),
 .UNSPECIFIED.,.F.,.F.)
B_SPLINE_CURVE_WITH_KNOTS((3,2,2,2,2,2,2,2,3),(0.1,0.125,0.15,0.175,0.2,
0.225,0.25,0.275,0.3),.UNSPECIFIED.)
CURVE()
GEOMETRIC_REPRESENTATION_ITEM()
RATIONAL_B_SPLINE_CURVE((1.,0.923879532511287,1.,0.923879532511287,1.,0.923879532511287,
1.,0.923879532511287,1.,0.923879532511287,1.,0.923879532511287,1.,0.923879532511287,
1.,0.923879532511287,1.))
REPRESENTATION_ITEM('')
);
#130=(
BOUNDED_CURVE()
B_SPLINE_CURVE(2,(#10037,#10038,#10039,#10040,#10041,#10042,#10043,#10044,
#10045,#10046,#10047,#10048,#10049,#10050,#10051,#10052,#10053),
 .UNSPECIFIED.,.F.,.F.)
B_SPLINE_CURVE_WITH_KNOTS((3,2,2,2,2,2,2,2,3),(0.1,0.125,0.15,0.175,0.2,
0.225,0.25,0.275,0.3),.UNSPECIFIED.)
CURVE()
GEOMETRIC_REPRESENTATION_ITEM()
RATIONAL_B_SPLINE_CURVE((1.,0.923879532511287,1.,0.923879532511287,1.,0.923879532511287,
1.,0.923879532511287,1.,0.923879532511287,1.,0.923879532511287,1.,0.923879532511287,
1.,0.923879532511287,1.))
REPRESENTATION_ITEM('')
);
#143=CONICAL_SURFACE('',#6105,2.008532,0.785398163397448);
#144=CONICAL_SURFACE('',#6108,2.5,0.785398163397448);
#145=CONICAL_SURFACE('',#6115,5.06,1.0471975511966);
#146=CONICAL_SURFACE('',#6117,2.5,0.785398163397448);
#147=CONICAL_SURFACE('',#6119,2.008532,0.785398163397448);
#155=SHAPE_REPRESENTATION_RELATIONSHIP('SRR','None',#10460,#163);
#163=ADVANCED_BREP_SHAPE_REPRESENTATION('',(#179),#10412);
#171=STYLED_ITEM('',(#10503),#179);
#179=MANIFOLD_SOLID_BREP('Body1',#5306);
#217=FACE_BOUND('',#882,.T.);
#218=FACE_BOUND('',#884,.T.);
#267=PLANE('',#6121);
#268=PLANE('',#6124);
#269=PLANE('',#6127);
#270=PLANE('',#6128);
#271=PLANE('',#6129);
#272=PLANE('',#6130);
#273=PLANE('',#6131);
#274=PLANE('',#6132);
#541=FACE_OUTER_BOUND('',#868,.T.);
#542=FACE_OUTER_BOUND('',#869,.T.);
#543=FACE_OUTER_BOUND('',#870,.T.);
#544=FACE_OUTER_BOUND('',#871,.T.);
#545=FACE_OUTER_BOUND('',#872,.T.);
#546=FACE_OUTER_BOUND('',#873,.T.);
#547=FACE_OUTER_BOUND('',#874,.T.);
#548=FACE_OUTER_BOUND('',#875,.T.);
#549=FACE_OUTER_BOUND('',#876,.T.);
#550=FACE_OUTER_BOUND('',#877,.T.);
#551=FACE_OUTER_BOUND('',#878,.T.);
#552=FACE_OUTER_BOUND('',#879,.T.);
#553=FACE_OUTER_BOUND('',#880,.T.);
#554=FACE_OUTER_BOUND('',#881,.T.);
#555=FACE_OUTER_BOUND('',#883,.T.);
#556=FACE_OUTER_BOUND('',#885,.T.);
#557=FACE_OUTER_BOUND('',#886,.T.);
#558=FACE_OUTER_BOUND('',#887,.T.);
#559=FACE_OUTER_BOUND('',#888,.T.);
#560=FACE_OUTER_BOUND('',#889,.T.);
#561=FACE_OUTER_BOUND('',#890,.T.);
#562=FACE_OUTER_BOUND('',#891,.T.);
#563=FACE_OUTER_BOUND('',#892,.T.);
#564=FACE_OUTER_BOUND('',#893,.T.);
#868=EDGE_LOOP('',(#4664,#4665,#4666,#4667));
#869=EDGE_LOOP('',(#4668,#4669,#4670,#4671));
#870=EDGE_LOOP('',(#4672,#4673,#4674,#4675));
#871=EDGE_LOOP('',(#4676,#4677,#4678,#4679));
#872=EDGE_LOOP('',(#4680,#4681,#4682,#4683));
#873=EDGE_LOOP('',(#4684,#4685,#4686,#4687,#4688));
#874=EDGE_LOOP('',(#4689,#4690,#4691,#4692));
#875=EDGE_LOOP('',(#4693,#4694,#4695,#4696));
#876=EDGE_LOOP('',(#4697,#4698,#4699,#4700));
#877=EDGE_LOOP('',(#4701,#4702,#4703,#4704));
#878=EDGE_LOOP('',(#4705,#4706,#4707,#4708,#4709,#4710,#4711,#4712,#4713,
#4714));
#879=EDGE_LOOP('',(#4715,#4716,#4717));
#880=EDGE_LOOP('',(#4718,#4719,#4720));
#881=EDGE_LOOP('',(#4721,#4722,#4723,#4724,#4725,#4726));
#882=EDGE_LOOP('',(#4727,#4728,#4729,#4730,#4731));
#883=EDGE_LOOP('',(#4732));
#884=EDGE_LOOP('',(#4733,#4734,#4735,#4736,#4737));
#885=EDGE_LOOP('',(#4738,#4739,#4740,#4741));
#886=EDGE_LOOP('',(#4742,#4743,#4744,#4745));
#887=EDGE_LOOP('',(#4746,#4747,#4748,#4749));
#888=EDGE_LOOP('',(#4750,#4751,#4752,#4753));
#889=EDGE_LOOP('',(#4754,#4755,#4756,#4757));
#890=EDGE_LOOP('',(#4758,#4759,#4760,#4761,#4762));
#891=EDGE_LOOP('',(#4763,#4764,#4765,#4766));
#892=EDGE_LOOP('',(#4767,#4768,#4769,#4770,#4771,#4772,#4773,#4774,#4775,
#4776,#4777,#4778,#4779));
#893=EDGE_LOOP('',(#4780,#4781,#4782,#4783,#4784,#4785,#4786,#4787,#4788,
#4789,#4790,#4791,#4792,#4793));
#1163=LINE('',#9472,#1454);
#1164=LINE('',#9503,#1455);
#1165=LINE('',#9541,#1456);
#1166=LINE('',#9579,#1457);
#1167=LINE('',#9602,#1458);
#1168=LINE('',#9622,#1459);
#1169=LINE('',#9655,#1460);
#1170=LINE('',#9723,#1461);
#1171=LINE('',#9799,#1462);
#1172=LINE('',#9910,#1463);
#1173=LINE('',#9992,#1464);
#1174=LINE('',#9994,#1465);
#1175=LINE('',#9996,#1466);
#1176=LINE('',#9998,#1467);
#1177=LINE('',#10000,#1468);
#1178=LINE('',#10001,#1469);
#1179=LINE('',#10008,#1470);
#1180=LINE('',#10009,#1471);
#1181=LINE('',#10011,#1472);
#1182=LINE('',#10013,#1473);
#1183=LINE('',#10015,#1474);
#1184=LINE('',#10017,#1475);
#1454=VECTOR('',#7827,2.54979787499999);
#1455=VECTOR('',#7832,2.54979787499999);
#1456=VECTOR('',#7835,2.54979787499999);
#1457=VECTOR('',#7838,2.54979787499999);
#1458=VECTOR('',#7843,2.008532);
#1459=VECTOR('',#7850,2.5);
#1460=VECTOR('',#7857,2.008532);
#1461=VECTOR('',#7860,2.008532);
#1462=VECTOR('',#7863,2.008532);
#1463=VECTOR('',#7868,5.06);
#1464=VECTOR('',#7881,1000.);
#1465=VECTOR('',#7882,1000.);
#1466=VECTOR('',#7883,1000.);
#1467=VECTOR('',#7884,1000.);
#1468=VECTOR('',#7885,1000.);
#1469=VECTOR('',#7886,1000.);
#1470=VECTOR('',#7899,1000.);
#1471=VECTOR('',#7900,1000.);
#1472=VECTOR('',#7903,1000.);
#1473=VECTOR('',#7906,1000.);
#1474=VECTOR('',#7909,1000.);
#1475=VECTOR('',#7912,1000.);
#1904=CIRCLE('',#6100,2.54979787499999);
#1905=CIRCLE('',#6104,2.54979787499999);
#1906=CIRCLE('',#6106,2.008532);
#1907=CIRCLE('',#6107,2.5);
#1908=CIRCLE('',#6109,2.008532);
#1909=CIRCLE('',#6110,2.5);
#1910=CIRCLE('',#6116,3.22);
#1911=CIRCLE('',#6118,2.5);
#1912=CIRCLE('',#6120,2.5);
#1913=CIRCLE('',#6122,2.54924752923115);
#1914=CIRCLE('',#6123,2.5195932879569);
#1915=CIRCLE('',#6125,2.54909484356462);
#1916=CIRCLE('',#6126,2.5196046498842);
#2393=VERTEX_POINT('',#9470);
#2394=VERTEX_POINT('',#9471);
#2395=VERTEX_POINT('',#9473);
#2396=VERTEX_POINT('',#9485);
#2397=VERTEX_POINT('',#9501);
#2398=VERTEX_POINT('',#9502);
#2399=VERTEX_POINT('',#9539);
#2400=VERTEX_POINT('',#9540);
#2401=VERTEX_POINT('',#9577);
#2402=VERTEX_POINT('',#9578);
#2403=VERTEX_POINT('',#9580);
#2404=VERTEX_POINT('',#9588);
#2405=VERTEX_POINT('',#9600);
#2406=VERTEX_POINT('',#9601);
#2407=VERTEX_POINT('',#9603);
#2408=VERTEX_POINT('',#9605);
#2409=VERTEX_POINT('',#9620);
#2410=VERTEX_POINT('',#9621);
#2411=VERTEX_POINT('',#9623);
#2412=VERTEX_POINT('',#9638);
#2413=VERTEX_POINT('',#9640);
#2414=VERTEX_POINT('',#9653);
#2415=VERTEX_POINT('',#9654);
#2416=VERTEX_POINT('',#9721);
#2417=VERTEX_POINT('',#9722);
#2418=VERTEX_POINT('',#9797);
#2419=VERTEX_POINT('',#9798);
#2420=VERTEX_POINT('',#9892);
#2421=VERTEX_POINT('',#9893);
#2422=VERTEX_POINT('',#9897);
#2423=VERTEX_POINT('',#9901);
#2424=VERTEX_POINT('',#9905);
#2425=VERTEX_POINT('',#9909);
#2426=VERTEX_POINT('',#9912);
#2427=VERTEX_POINT('',#9916);
#2428=VERTEX_POINT('',#9924);
#2429=VERTEX_POINT('',#9953);
#2430=VERTEX_POINT('',#9990);
#2431=VERTEX_POINT('',#9991);
#2432=VERTEX_POINT('',#9993);
#2433=VERTEX_POINT('',#9995);
#2434=VERTEX_POINT('',#9997);
#2435=VERTEX_POINT('',#9999);
#3157=EDGE_CURVE('',#2393,#2394,#1163,.T.);
#3158=EDGE_CURVE('',#2394,#2395,#114,.T.);
#3159=EDGE_CURVE('',#2395,#2396,#1904,.T.);
#3160=EDGE_CURVE('',#2393,#2396,#115,.T.);
#3161=EDGE_CURVE('',#2397,#2398,#1164,.T.);
#3162=EDGE_CURVE('',#2398,#2394,#116,.T.);
#3163=EDGE_CURVE('',#2397,#2393,#117,.T.);
#3164=EDGE_CURVE('',#2399,#2400,#1165,.T.);
#3165=EDGE_CURVE('',#2400,#2398,#118,.T.);
#3166=EDGE_CURVE('',#2399,#2397,#119,.T.);
#3167=EDGE_CURVE('',#2401,#2402,#1166,.T.);
#3168=EDGE_CURVE('',#2403,#2401,#120,.T.);
#3169=EDGE_CURVE('',#2403,#2404,#1905,.T.);
#3170=EDGE_CURVE('',#2404,#2402,#121,.T.);
#3171=EDGE_CURVE('',#2405,#2406,#1167,.T.);
#3172=EDGE_CURVE('',#2407,#2405,#1906,.T.);
#3173=EDGE_CURVE('',#2407,#2408,#77,.T.);
#3174=EDGE_CURVE('',#2408,#2406,#1907,.T.);
#3175=EDGE_CURVE('',#2409,#2410,#1168,.T.);
#3176=EDGE_CURVE('',#2409,#2411,#78,.T.);
#3177=EDGE_CURVE('',#2411,#2412,#1908,.T.);
#3178=EDGE_CURVE('',#2412,#2413,#79,.T.);
#3179=EDGE_CURVE('',#2410,#2413,#1909,.T.);
#3180=EDGE_CURVE('',#2414,#2415,#1169,.T.);
#3181=EDGE_CURVE('',#2407,#2415,#80,.F.);
#3182=EDGE_CURVE('',#2405,#2414,#81,.T.);
#3183=EDGE_CURVE('',#2416,#2417,#1170,.T.);
#3184=EDGE_CURVE('',#2415,#2417,#82,.F.);
#3185=EDGE_CURVE('',#2414,#2416,#83,.T.);
#3186=EDGE_CURVE('',#2418,#2419,#1171,.T.);
#3187=EDGE_CURVE('',#2418,#2412,#84,.T.);
#3188=EDGE_CURVE('',#2419,#2411,#85,.F.);
#3189=EDGE_CURVE('',#2417,#2419,#86,.F.);
#3190=EDGE_CURVE('',#2416,#2418,#87,.T.);
#3191=EDGE_CURVE('',#2420,#2421,#122,.T.);
#3192=EDGE_CURVE('',#2422,#2420,#123,.T.);
#3193=EDGE_CURVE('',#2423,#2422,#124,.T.);
#3194=EDGE_CURVE('',#2424,#2423,#125,.F.);
#3195=EDGE_CURVE('',#2424,#2425,#1172,.T.);
#3196=EDGE_CURVE('',#2425,#2425,#1910,.T.);
#3197=EDGE_CURVE('',#2426,#2424,#126,.F.);
#3198=EDGE_CURVE('',#2427,#2426,#127,.T.);
#3199=EDGE_CURVE('',#2421,#2427,#128,.T.);
#3200=EDGE_CURVE('',#2428,#2410,#1911,.T.);
#3201=EDGE_CURVE('',#2428,#2409,#88,.T.);
#3202=EDGE_CURVE('',#2406,#2429,#1912,.T.);
#3203=EDGE_CURVE('',#2429,#2405,#89,.F.);
#3204=EDGE_CURVE('',#2430,#2431,#1173,.T.);
#3205=EDGE_CURVE('',#2431,#2432,#1174,.T.);
#3206=EDGE_CURVE('',#2432,#2433,#1175,.T.);
#3207=EDGE_CURVE('',#2433,#2434,#1176,.T.);
#3208=EDGE_CURVE('',#2434,#2435,#1177,.T.);
#3209=EDGE_CURVE('',#2435,#2430,#1178,.T.);
#3210=EDGE_CURVE('',#2396,#2413,#1913,.T.);
#3211=EDGE_CURVE('',#2428,#2395,#1914,.T.);
#3212=EDGE_CURVE('',#2429,#2403,#1915,.T.);
#3213=EDGE_CURVE('',#2404,#2408,#1916,.T.);
#3214=EDGE_CURVE('',#2426,#2431,#1179,.T.);
#3215=EDGE_CURVE('',#2427,#2430,#1180,.T.);
#3216=EDGE_CURVE('',#2421,#2435,#1181,.T.);
#3217=EDGE_CURVE('',#2420,#2434,#1182,.T.);
#3218=EDGE_CURVE('',#2422,#2433,#1183,.T.);
#3219=EDGE_CURVE('',#2423,#2432,#1184,.T.);
#3220=EDGE_CURVE('',#2402,#2400,#129,.T.);
#3221=EDGE_CURVE('',#2401,#2399,#130,.T.);
#4664=ORIENTED_EDGE('',*,*,#3157,.T.);
#4665=ORIENTED_EDGE('',*,*,#3158,.T.);
#4666=ORIENTED_EDGE('',*,*,#3159,.T.);
#4667=ORIENTED_EDGE('',*,*,#3160,.F.);
#4668=ORIENTED_EDGE('',*,*,#3161,.T.);
#4669=ORIENTED_EDGE('',*,*,#3162,.T.);
#4670=ORIENTED_EDGE('',*,*,#3157,.F.);
#4671=ORIENTED_EDGE('',*,*,#3163,.F.);
#4672=ORIENTED_EDGE('',*,*,#3164,.T.);
#4673=ORIENTED_EDGE('',*,*,#3165,.T.);
#4674=ORIENTED_EDGE('',*,*,#3161,.F.);
#4675=ORIENTED_EDGE('',*,*,#3166,.F.);
#4676=ORIENTED_EDGE('',*,*,#3167,.F.);
#4677=ORIENTED_EDGE('',*,*,#3168,.F.);
#4678=ORIENTED_EDGE('',*,*,#3169,.T.);
#4679=ORIENTED_EDGE('',*,*,#3170,.T.);
#4680=ORIENTED_EDGE('',*,*,#3171,.F.);
#4681=ORIENTED_EDGE('',*,*,#3172,.F.);
#4682=ORIENTED_EDGE('',*,*,#3173,.T.);
#4683=ORIENTED_EDGE('',*,*,#3174,.T.);
#4684=ORIENTED_EDGE('',*,*,#3175,.F.);
#4685=ORIENTED_EDGE('',*,*,#3176,.T.);
#4686=ORIENTED_EDGE('',*,*,#3177,.T.);
#4687=ORIENTED_EDGE('',*,*,#3178,.T.);
#4688=ORIENTED_EDGE('',*,*,#3179,.F.);
#4689=ORIENTED_EDGE('',*,*,#3180,.T.);
#4690=ORIENTED_EDGE('',*,*,#3181,.F.);
#4691=ORIENTED_EDGE('',*,*,#3172,.T.);
#4692=ORIENTED_EDGE('',*,*,#3182,.T.);
#4693=ORIENTED_EDGE('',*,*,#3183,.T.);
#4694=ORIENTED_EDGE('',*,*,#3184,.F.);
#4695=ORIENTED_EDGE('',*,*,#3180,.F.);
#4696=ORIENTED_EDGE('',*,*,#3185,.T.);
#4697=ORIENTED_EDGE('',*,*,#3186,.F.);
#4698=ORIENTED_EDGE('',*,*,#3187,.T.);
#4699=ORIENTED_EDGE('',*,*,#3177,.F.);
#4700=ORIENTED_EDGE('',*,*,#3188,.F.);
#4701=ORIENTED_EDGE('',*,*,#3186,.T.);
#4702=ORIENTED_EDGE('',*,*,#3189,.F.);
#4703=ORIENTED_EDGE('',*,*,#3183,.F.);
#4704=ORIENTED_EDGE('',*,*,#3190,.T.);
#4705=ORIENTED_EDGE('',*,*,#3191,.F.);
#4706=ORIENTED_EDGE('',*,*,#3192,.F.);
#4707=ORIENTED_EDGE('',*,*,#3193,.F.);
#4708=ORIENTED_EDGE('',*,*,#3194,.F.);
#4709=ORIENTED_EDGE('',*,*,#3195,.T.);
#4710=ORIENTED_EDGE('',*,*,#3196,.F.);
#4711=ORIENTED_EDGE('',*,*,#3195,.F.);
#4712=ORIENTED_EDGE('',*,*,#3197,.F.);
#4713=ORIENTED_EDGE('',*,*,#3198,.F.);
#4714=ORIENTED_EDGE('',*,*,#3199,.F.);
#4715=ORIENTED_EDGE('',*,*,#3175,.T.);
#4716=ORIENTED_EDGE('',*,*,#3200,.F.);
#4717=ORIENTED_EDGE('',*,*,#3201,.T.);
#4718=ORIENTED_EDGE('',*,*,#3171,.T.);
#4719=ORIENTED_EDGE('',*,*,#3202,.T.);
#4720=ORIENTED_EDGE('',*,*,#3203,.T.);
#4721=ORIENTED_EDGE('',*,*,#3204,.T.);
#4722=ORIENTED_EDGE('',*,*,#3205,.T.);
#4723=ORIENTED_EDGE('',*,*,#3206,.T.);
#4724=ORIENTED_EDGE('',*,*,#3207,.T.);
#4725=ORIENTED_EDGE('',*,*,#3208,.T.);
#4726=ORIENTED_EDGE('',*,*,#3209,.T.);
#4727=ORIENTED_EDGE('',*,*,#3210,.F.);
#4728=ORIENTED_EDGE('',*,*,#3159,.F.);
#4729=ORIENTED_EDGE('',*,*,#3211,.F.);
#4730=ORIENTED_EDGE('',*,*,#3200,.T.);
#4731=ORIENTED_EDGE('',*,*,#3179,.T.);
#4732=ORIENTED_EDGE('',*,*,#3196,.T.);
#4733=ORIENTED_EDGE('',*,*,#3212,.F.);
#4734=ORIENTED_EDGE('',*,*,#3202,.F.);
#4735=ORIENTED_EDGE('',*,*,#3174,.F.);
#4736=ORIENTED_EDGE('',*,*,#3213,.F.);
#4737=ORIENTED_EDGE('',*,*,#3169,.F.);
#4738=ORIENTED_EDGE('',*,*,#3198,.T.);
#4739=ORIENTED_EDGE('',*,*,#3214,.T.);
#4740=ORIENTED_EDGE('',*,*,#3204,.F.);
#4741=ORIENTED_EDGE('',*,*,#3215,.F.);
#4742=ORIENTED_EDGE('',*,*,#3199,.T.);
#4743=ORIENTED_EDGE('',*,*,#3215,.T.);
#4744=ORIENTED_EDGE('',*,*,#3209,.F.);
#4745=ORIENTED_EDGE('',*,*,#3216,.F.);
#4746=ORIENTED_EDGE('',*,*,#3191,.T.);
#4747=ORIENTED_EDGE('',*,*,#3216,.T.);
#4748=ORIENTED_EDGE('',*,*,#3208,.F.);
#4749=ORIENTED_EDGE('',*,*,#3217,.F.);
#4750=ORIENTED_EDGE('',*,*,#3192,.T.);
#4751=ORIENTED_EDGE('',*,*,#3217,.T.);
#4752=ORIENTED_EDGE('',*,*,#3207,.F.);
#4753=ORIENTED_EDGE('',*,*,#3218,.F.);
#4754=ORIENTED_EDGE('',*,*,#3193,.T.);
#4755=ORIENTED_EDGE('',*,*,#3218,.T.);
#4756=ORIENTED_EDGE('',*,*,#3206,.F.);
#4757=ORIENTED_EDGE('',*,*,#3219,.F.);
#4758=ORIENTED_EDGE('',*,*,#3197,.T.);
#4759=ORIENTED_EDGE('',*,*,#3194,.T.);
#4760=ORIENTED_EDGE('',*,*,#3219,.T.);
#4761=ORIENTED_EDGE('',*,*,#3205,.F.);
#4762=ORIENTED_EDGE('',*,*,#3214,.F.);
#4763=ORIENTED_EDGE('',*,*,#3167,.T.);
#4764=ORIENTED_EDGE('',*,*,#3220,.T.);
#4765=ORIENTED_EDGE('',*,*,#3164,.F.);
#4766=ORIENTED_EDGE('',*,*,#3221,.F.);
#4767=ORIENTED_EDGE('',*,*,#3212,.T.);
#4768=ORIENTED_EDGE('',*,*,#3168,.T.);
#4769=ORIENTED_EDGE('',*,*,#3221,.T.);
#4770=ORIENTED_EDGE('',*,*,#3166,.T.);
#4771=ORIENTED_EDGE('',*,*,#3163,.T.);
#4772=ORIENTED_EDGE('',*,*,#3160,.T.);
#4773=ORIENTED_EDGE('',*,*,#3210,.T.);
#4774=ORIENTED_EDGE('',*,*,#3178,.F.);
#4775=ORIENTED_EDGE('',*,*,#3187,.F.);
#4776=ORIENTED_EDGE('',*,*,#3190,.F.);
#4777=ORIENTED_EDGE('',*,*,#3185,.F.);
#4778=ORIENTED_EDGE('',*,*,#3182,.F.);
#4779=ORIENTED_EDGE('',*,*,#3203,.F.);
#4780=ORIENTED_EDGE('',*,*,#3213,.T.);
#4781=ORIENTED_EDGE('',*,*,#3173,.F.);
#4782=ORIENTED_EDGE('',*,*,#3181,.T.);
#4783=ORIENTED_EDGE('',*,*,#3184,.T.);
#4784=ORIENTED_EDGE('',*,*,#3189,.T.);
#4785=ORIENTED_EDGE('',*,*,#3188,.T.);
#4786=ORIENTED_EDGE('',*,*,#3176,.F.);
#4787=ORIENTED_EDGE('',*,*,#3201,.F.);
#4788=ORIENTED_EDGE('',*,*,#3211,.T.);
#4789=ORIENTED_EDGE('',*,*,#3158,.F.);
#4790=ORIENTED_EDGE('',*,*,#3162,.F.);
#4791=ORIENTED_EDGE('',*,*,#3165,.F.);
#4792=ORIENTED_EDGE('',*,*,#3220,.F.);
#4793=ORIENTED_EDGE('',*,*,#3170,.F.);
#5000=CYLINDRICAL_SURFACE('',#6099,2.54979787499999);
#5001=CYLINDRICAL_SURFACE('',#6101,2.54979787499999);
#5002=CYLINDRICAL_SURFACE('',#6102,2.54979787499999);
#5003=CYLINDRICAL_SURFACE('',#6103,2.54979787499999);
#5004=CYLINDRICAL_SURFACE('',#6111,2.008532);
#5005=CYLINDRICAL_SURFACE('',#6112,2.008532);
#5006=CYLINDRICAL_SURFACE('',#6113,2.008532);
#5007=CYLINDRICAL_SURFACE('',#6114,2.008532);
#5008=CYLINDRICAL_SURFACE('',#6133,2.54979787499999);
#5275=ADVANCED_FACE('',(#541),#5000,.F.);
#5276=ADVANCED_FACE('',(#542),#5001,.F.);
#5277=ADVANCED_FACE('',(#543),#5002,.F.);
#5278=ADVANCED_FACE('',(#544),#5003,.F.);
#5279=ADVANCED_FACE('',(#545),#143,.F.);
#5280=ADVANCED_FACE('',(#546),#144,.F.);
#5281=ADVANCED_FACE('',(#547),#5004,.F.);
#5282=ADVANCED_FACE('',(#548),#5005,.F.);
#5283=ADVANCED_FACE('',(#549),#5006,.F.);
#5284=ADVANCED_FACE('',(#550),#5007,.F.);
#5285=ADVANCED_FACE('',(#551),#145,.T.);
#5286=ADVANCED_FACE('',(#552),#146,.F.);
#5287=ADVANCED_FACE('',(#553),#147,.F.);
#5288=ADVANCED_FACE('',(#554,#217),#267,.F.);
#5289=ADVANCED_FACE('',(#555,#218),#268,.F.);
#5290=ADVANCED_FACE('',(#556),#269,.T.);
#5291=ADVANCED_FACE('',(#557),#270,.T.);
#5292=ADVANCED_FACE('',(#558),#271,.T.);
#5293=ADVANCED_FACE('',(#559),#272,.T.);
#5294=ADVANCED_FACE('',(#560),#273,.T.);
#5295=ADVANCED_FACE('',(#561),#274,.T.);
#5296=ADVANCED_FACE('',(#562),#5008,.F.);
#5297=ADVANCED_FACE('',(#563),#75,.T.);
#5298=ADVANCED_FACE('',(#564),#76,.T.);
#5306=CLOSED_SHELL('',(#5275,#5276,#5277,#5278,#5279,#5280,#5281,#5282,
#5283,#5284,#5285,#5286,#5287,#5288,#5289,#5290,#5291,#5292,#5293,#5294,
#5295,#5296,#5297,#5298));
#6098=AXIS2_PLACEMENT_3D('',#9468,#7823,#7824);
#6099=AXIS2_PLACEMENT_3D('',#9469,#7825,#7826);
#6100=AXIS2_PLACEMENT_3D('',#9486,#7828,#7829);
#6101=AXIS2_PLACEMENT_3D('',#9500,#7830,#7831);
#6102=AXIS2_PLACEMENT_3D('',#9538,#7833,#7834);
#6103=AXIS2_PLACEMENT_3D('',#9576,#7836,#7837);
#6104=AXIS2_PLACEMENT_3D('',#9589,#7839,#7840);
#6105=AXIS2_PLACEMENT_3D('',#9599,#7841,#7842);
#6106=AXIS2_PLACEMENT_3D('',#9604,#7844,#7845);
#6107=AXIS2_PLACEMENT_3D('',#9618,#7846,#7847);
#6108=AXIS2_PLACEMENT_3D('',#9619,#7848,#7849);
#6109=AXIS2_PLACEMENT_3D('',#9639,#7851,#7852);
#6110=AXIS2_PLACEMENT_3D('',#9651,#7853,#7854);
#6111=AXIS2_PLACEMENT_3D('',#9652,#7855,#7856);
#6112=AXIS2_PLACEMENT_3D('',#9720,#7858,#7859);
#6113=AXIS2_PLACEMENT_3D('',#9796,#7861,#7862);
#6114=AXIS2_PLACEMENT_3D('',#9818,#7864,#7865);
#6115=AXIS2_PLACEMENT_3D('',#9891,#7866,#7867);
#6116=AXIS2_PLACEMENT_3D('',#9911,#7869,#7870);
#6117=AXIS2_PLACEMENT_3D('',#9923,#7871,#7872);
#6118=AXIS2_PLACEMENT_3D('',#9925,#7873,#7874);
#6119=AXIS2_PLACEMENT_3D('',#9952,#7875,#7876);
#6120=AXIS2_PLACEMENT_3D('',#9954,#7877,#7878);
#6121=AXIS2_PLACEMENT_3D('',#9989,#7879,#7880);
#6122=AXIS2_PLACEMENT_3D('',#10002,#7887,#7888);
#6123=AXIS2_PLACEMENT_3D('',#10003,#7889,#7890);
#6124=AXIS2_PLACEMENT_3D('',#10004,#7891,#7892);
#6125=AXIS2_PLACEMENT_3D('',#10005,#7893,#7894);
#6126=AXIS2_PLACEMENT_3D('',#10006,#7895,#7896);
#6127=AXIS2_PLACEMENT_3D('',#10007,#7897,#7898);
#6128=AXIS2_PLACEMENT_3D('',#10010,#7901,#7902);
#6129=AXIS2_PLACEMENT_3D('',#10012,#7904,#7905);
#6130=AXIS2_PLACEMENT_3D('',#10014,#7907,#7908);
#6131=AXIS2_PLACEMENT_3D('',#10016,#7910,#7911);
#6132=AXIS2_PLACEMENT_3D('',#10018,#7913,#7914);
#6133=AXIS2_PLACEMENT_3D('',#10019,#7915,#7916);
#7823=DIRECTION('axis',(0.,0.,1.));
#7824=DIRECTION('refdir',(1.,0.,0.));
#7825=DIRECTION('center_axis',(-1.,0.,0.));
#7826=DIRECTION('ref_axis',(0.,-2.66671190320869E-15,-1.));
#7827=DIRECTION('',(1.,0.,0.));
#7828=DIRECTION('center_axis',(1.,0.,0.));
#7829=DIRECTION('ref_axis',(0.,-2.66671190320869E-15,-1.));
#7830=DIRECTION('center_axis',(-1.,0.,0.));
#7831=DIRECTION('ref_axis',(0.,-2.66671190320869E-15,-1.));
#7832=DIRECTION('',(1.,0.,0.));
#7833=DIRECTION('center_axis',(-1.,0.,0.));
#7834=DIRECTION('ref_axis',(0.,-2.66671190320869E-15,-1.));
#7835=DIRECTION('',(1.,0.,0.));
#7836=DIRECTION('center_axis',(-1.,0.,0.));
#7837=DIRECTION('ref_axis',(0.,-2.66671190320869E-15,-1.));
#7838=DIRECTION('',(1.,0.,0.));
#7839=DIRECTION('center_axis',(-1.,0.,0.));
#7840=DIRECTION('ref_axis',(0.,-2.66671190320869E-15,-1.));
#7841=DIRECTION('center_axis',(-1.,0.,0.));
#7842=DIRECTION('ref_axis',(0.,0.,1.));
#7843=DIRECTION('',(-0.707106781186548,-8.65956056235493E-17,-0.707106781186547));
#7844=DIRECTION('center_axis',(-1.,0.,0.));
#7845=DIRECTION('ref_axis',(0.,0.,1.));
#7846=DIRECTION('center_axis',(-1.,0.,0.));
#7847=DIRECTION('ref_axis',(0.,0.,1.));
#7848=DIRECTION('center_axis',(1.,0.,0.));
#7849=DIRECTION('ref_axis',(0.,0.,-1.));
#7850=DIRECTION('',(0.707106781186548,-8.65956056235493E-17,0.707106781186547));
#7851=DIRECTION('center_axis',(-1.,0.,0.));
#7852=DIRECTION('ref_axis',(0.,0.,1.));
#7853=DIRECTION('center_axis',(-1.,0.,0.));
#7854=DIRECTION('ref_axis',(0.,0.,1.));
#7855=DIRECTION('center_axis',(-1.,0.,0.));
#7856=DIRECTION('ref_axis',(0.,0.,1.));
#7857=DIRECTION('',(-1.,0.,0.));
#7858=DIRECTION('center_axis',(-1.,0.,0.));
#7859=DIRECTION('ref_axis',(0.,0.,1.));
#7860=DIRECTION('',(-1.,0.,0.));
#7861=DIRECTION('center_axis',(-1.,0.,0.));
#7862=DIRECTION('ref_axis',(0.,0.,1.));
#7863=DIRECTION('',(-1.,0.,0.));
#7864=DIRECTION('center_axis',(-1.,0.,0.));
#7865=DIRECTION('ref_axis',(0.,0.,1.));
#7866=DIRECTION('center_axis',(1.,0.,0.));
#7867=DIRECTION('ref_axis',(0.,0.,-1.));
#7868=DIRECTION('',(-0.5,1.06057523872491E-16,-0.866025403784439));
#7869=DIRECTION('center_axis',(-1.,0.,0.));
#7870=DIRECTION('ref_axis',(0.,0.,1.));
#7871=DIRECTION('center_axis',(1.,0.,0.));
#7872=DIRECTION('ref_axis',(0.,0.,-1.));
#7873=DIRECTION('center_axis',(-1.,0.,0.));
#7874=DIRECTION('ref_axis',(0.,0.,1.));
#7875=DIRECTION('center_axis',(-1.,0.,0.));
#7876=DIRECTION('ref_axis',(0.,0.,1.));
#7877=DIRECTION('center_axis',(-1.,0.,0.));
#7878=DIRECTION('ref_axis',(0.,0.,1.));
#7879=DIRECTION('center_axis',(-1.,0.,0.));
#7880=DIRECTION('ref_axis',(0.,0.,1.));
#7881=DIRECTION('',(0.,-0.5,0.866025403784439));
#7882=DIRECTION('',(0.,-1.,0.));
#7883=DIRECTION('',(0.,-0.5,-0.866025403784439));
#7884=DIRECTION('',(0.,0.5,-0.866025403784439));
#7885=DIRECTION('',(0.,1.,0.));
#7886=DIRECTION('',(0.,0.5,0.866025403784439));
#7887=DIRECTION('center_axis',(0.999999998812523,4.82472814902002E-5,-6.86688143352015E-6));
#7888=DIRECTION('ref_axis',(-4.8541881071249E-5,0.998613318949696,-0.0526444380724065));
#7889=DIRECTION('center_axis',(0.999999999837215,-4.38888781624564E-6,1.75016240224852E-5));
#7890=DIRECTION('ref_axis',(1.79722394331351E-5,0.32841963521485,-0.944531917344429));
#7891=DIRECTION('center_axis',(1.,0.,0.));
#7892=DIRECTION('ref_axis',(0.,0.,-1.));
#7893=DIRECTION('center_axis',(-0.999999999904602,-1.36751150609827E-5,
1.94633545137007E-6));
#7894=DIRECTION('ref_axis',(-1.37586092717476E-5,0.973645618966202,-0.228066237042274));
#7895=DIRECTION('center_axis',(-0.999999999786601,5.02509006274664E-6,-2.00386156144365E-5));
#7896=DIRECTION('ref_axis',(2.05774510033662E-5,0.156136104303204,-0.9877355498865));
#7897=DIRECTION('center_axis',(0.,0.866025403784439,0.5));
#7898=DIRECTION('ref_axis',(0.,-0.5,0.866025403784439));
#7899=DIRECTION('',(1.,0.,0.));
#7900=DIRECTION('',(1.,0.,0.));
#7901=DIRECTION('center_axis',(0.,0.866025403784439,-0.5));
#7902=DIRECTION('ref_axis',(0.,0.5,0.866025403784439));
#7903=DIRECTION('',(1.,0.,0.));
#7904=DIRECTION('center_axis',(0.,0.,-1.));
#7905=DIRECTION('ref_axis',(-1.,0.,0.));
#7906=DIRECTION('',(1.,0.,0.));
#7907=DIRECTION('center_axis',(0.,-0.866025403784439,-0.5));
#7908=DIRECTION('ref_axis',(0.,0.5,-0.866025403784439));
#7909=DIRECTION('',(1.,0.,0.));
#7910=DIRECTION('center_axis',(0.,-0.866025403784439,0.5));
#7911=DIRECTION('ref_axis',(0.,-0.5,-0.866025403784439));
#7912=DIRECTION('',(1.,0.,0.));
#7913=DIRECTION('center_axis',(0.,0.,1.));
#7914=DIRECTION('ref_axis',(1.,0.,0.));
#7915=DIRECTION('center_axis',(-1.,0.,0.));
#7916=DIRECTION('ref_axis',(0.,-2.66671190320869E-15,-1.));
#9468=CARTESIAN_POINT('',(0.,0.,0.));
#9469=CARTESIAN_POINT('Origin',(-4.1335320013656,6.79957634403871E-15,-6.66133814775094E-15));
#9470=CARTESIAN_POINT('',(-0.696032001365594,7.11183652464788E-15,2.549797875));
#9471=CARTESIAN_POINT('',(-0.571032001365594,7.11183652464788E-15,2.549797875));
#9472=CARTESIAN_POINT('',(-4.1335320013656,1.39114128686866E-14,2.54979787499999));
#9473=CARTESIAN_POINT('',(8.51787316660525E-16,1.09749718660244,-2.30151452933807));
#9474=CARTESIAN_POINT('Ctrl Pts',(-0.571032001365594,3.12260180609148E-16,
2.549797875));
#9475=CARTESIAN_POINT('Ctrl Pts',(-0.508532001365594,-1.0561608611351,2.549797875));
#9476=CARTESIAN_POINT('Ctrl Pts',(-0.446032001365594,-1.80297936806755,
1.80297936806755));
#9477=CARTESIAN_POINT('Ctrl Pts',(-0.383532001365594,-2.549797875,1.0561608611351));
#9478=CARTESIAN_POINT('Ctrl Pts',(-0.321032001365594,-2.549797875,4.68390270913721E-16));
#9479=CARTESIAN_POINT('Ctrl Pts',(-0.258532001365594,-2.549797875,-1.0561608611351));
#9480=CARTESIAN_POINT('Ctrl Pts',(-0.196032001365594,-1.80297936806755,
-1.80297936806755));
#9481=CARTESIAN_POINT('Ctrl Pts',(-0.133532001365594,-1.0561608611351,-2.549797875));
#9482=CARTESIAN_POINT('Ctrl Pts',(-0.0710320013655938,0.,-2.549797875));
#9483=CARTESIAN_POINT('Ctrl Pts',(-0.0368970038158504,0.576832774511702,
-2.549797875));
#9484=CARTESIAN_POINT('Ctrl Pts',(8.51787316660525E-16,1.09749718660244,
-2.30151452933807));
#9485=CARTESIAN_POINT('',(1.55011212503014E-14,2.40346423367414,-0.851368827714362));
#9486=CARTESIAN_POINT('Origin',(0.,6.79957634403871E-15,-6.66133814775094E-15));
#9487=CARTESIAN_POINT('Ctrl Pts',(-0.696032001365594,3.12260180609148E-16,
2.549797875));
#9488=CARTESIAN_POINT('Ctrl Pts',(-0.633532001365594,-1.0561608611351,2.549797875));
#9489=CARTESIAN_POINT('Ctrl Pts',(-0.571032001365594,-1.80297936806755,
1.80297936806755));
#9490=CARTESIAN_POINT('Ctrl Pts',(-0.508532001365594,-2.549797875,1.0561608611351));
#9491=CARTESIAN_POINT('Ctrl Pts',(-0.446032001365594,-2.549797875,4.68390270913721E-16));
#9492=CARTESIAN_POINT('Ctrl Pts',(-0.383532001365594,-2.549797875,-1.0561608611351));
#9493=CARTESIAN_POINT('Ctrl Pts',(-0.321032001365594,-1.80297936806755,
-1.80297936806755));
#9494=CARTESIAN_POINT('Ctrl Pts',(-0.258532001365594,-1.0561608611351,-2.549797875));
#9495=CARTESIAN_POINT('Ctrl Pts',(-0.196032001365594,0.,-2.549797875));
#9496=CARTESIAN_POINT('Ctrl Pts',(-0.133532001365594,1.0561608611351,-2.549797875));
#9497=CARTESIAN_POINT('Ctrl Pts',(-0.0710320013655938,1.80297936806755,
-1.80297936806755));
#9498=CARTESIAN_POINT('Ctrl Pts',(-0.0368970038158433,2.21086173453551,
-1.39509700159959));
#9499=CARTESIAN_POINT('Ctrl Pts',(1.55011212503014E-14,2.40346423367414,
-0.851368827714362));
#9500=CARTESIAN_POINT('Origin',(-4.1335320013656,6.79957634403871E-15,-6.66133814775094E-15));
#9501=CARTESIAN_POINT('',(-1.69603200136559,7.11183652464788E-15,2.549797875));
#9502=CARTESIAN_POINT('',(-1.5710320013656,7.11183652464788E-15,2.549797875));
#9503=CARTESIAN_POINT('',(-4.1335320013656,1.39114128686866E-14,2.54979787499999));
#9504=CARTESIAN_POINT('Ctrl Pts',(-1.5710320013656,3.12260180609148E-16,
2.549797875));
#9505=CARTESIAN_POINT('Ctrl Pts',(-1.50853200136559,-1.0561608611351,2.549797875));
#9506=CARTESIAN_POINT('Ctrl Pts',(-1.44603200136559,-1.80297936806755,1.80297936806755));
#9507=CARTESIAN_POINT('Ctrl Pts',(-1.38353200136559,-2.549797875,1.0561608611351));
#9508=CARTESIAN_POINT('Ctrl Pts',(-1.32103200136559,-2.549797875,4.68390270913721E-16));
#9509=CARTESIAN_POINT('Ctrl Pts',(-1.2585320013656,-2.549797875,-1.0561608611351));
#9510=CARTESIAN_POINT('Ctrl Pts',(-1.19603200136559,-1.80297936806755,-1.80297936806755));
#9511=CARTESIAN_POINT('Ctrl Pts',(-1.13353200136559,-1.0561608611351,-2.549797875));
#9512=CARTESIAN_POINT('Ctrl Pts',(-1.07103200136559,0.,-2.549797875));
#9513=CARTESIAN_POINT('Ctrl Pts',(-1.00853200136559,1.0561608611351,-2.549797875));
#9514=CARTESIAN_POINT('Ctrl Pts',(-0.946032001365594,1.80297936806755,-1.80297936806755));
#9515=CARTESIAN_POINT('Ctrl Pts',(-0.883532001365593,2.549797875,-1.0561608611351));
#9516=CARTESIAN_POINT('Ctrl Pts',(-0.821032001365594,2.549797875,-1.56130090304574E-16));
#9517=CARTESIAN_POINT('Ctrl Pts',(-0.758532001365594,2.549797875,1.0561608611351));
#9518=CARTESIAN_POINT('Ctrl Pts',(-0.696032001365594,1.80297936806755,1.80297936806755));
#9519=CARTESIAN_POINT('Ctrl Pts',(-0.633532001365594,1.0561608611351,2.549797875));
#9520=CARTESIAN_POINT('Ctrl Pts',(-0.571032001365594,3.12260180609148E-16,
2.549797875));
#9521=CARTESIAN_POINT('Ctrl Pts',(-1.69603200136559,3.12260180609148E-16,
2.549797875));
#9522=CARTESIAN_POINT('Ctrl Pts',(-1.63353200136559,-1.0561608611351,2.549797875));
#9523=CARTESIAN_POINT('Ctrl Pts',(-1.5710320013656,-1.80297936806755,1.80297936806755));
#9524=CARTESIAN_POINT('Ctrl Pts',(-1.50853200136559,-2.549797875,1.0561608611351));
#9525=CARTESIAN_POINT('Ctrl Pts',(-1.44603200136559,-2.549797875,4.68390270913721E-16));
#9526=CARTESIAN_POINT('Ctrl Pts',(-1.38353200136559,-2.549797875,-1.0561608611351));
#9527=CARTESIAN_POINT('Ctrl Pts',(-1.32103200136559,-1.80297936806755,-1.80297936806755));
#9528=CARTESIAN_POINT('Ctrl Pts',(-1.2585320013656,-1.0561608611351,-2.549797875));
#9529=CARTESIAN_POINT('Ctrl Pts',(-1.19603200136559,0.,-2.549797875));
#9530=CARTESIAN_POINT('Ctrl Pts',(-1.13353200136559,1.0561608611351,-2.549797875));
#9531=CARTESIAN_POINT('Ctrl Pts',(-1.07103200136559,1.80297936806755,-1.80297936806755));
#9532=CARTESIAN_POINT('Ctrl Pts',(-1.00853200136559,2.549797875,-1.0561608611351));
#9533=CARTESIAN_POINT('Ctrl Pts',(-0.946032001365594,2.549797875,-1.56130090304574E-16));
#9534=CARTESIAN_POINT('Ctrl Pts',(-0.883532001365594,2.549797875,1.0561608611351));
#9535=CARTESIAN_POINT('Ctrl Pts',(-0.821032001365594,1.80297936806755,1.80297936806755));
#9536=CARTESIAN_POINT('Ctrl Pts',(-0.758532001365594,1.0561608611351,2.549797875));
#9537=CARTESIAN_POINT('Ctrl Pts',(-0.696032001365594,3.12260180609148E-16,
2.549797875));
#9538=CARTESIAN_POINT('Origin',(-4.1335320013656,6.79957634403871E-15,-6.66133814775094E-15));
#9539=CARTESIAN_POINT('',(-2.6960320013656,7.11183652464788E-15,2.549797875));
#9540=CARTESIAN_POINT('',(-2.5710320013656,7.11183652464788E-15,2.549797875));
#9541=CARTESIAN_POINT('',(-4.1335320013656,1.39114128686866E-14,2.54979787499999));
#9542=CARTESIAN_POINT('Ctrl Pts',(-2.5710320013656,3.12260180609148E-16,
2.549797875));
#9543=CARTESIAN_POINT('Ctrl Pts',(-2.5085320013656,-1.0561608611351,2.549797875));
#9544=CARTESIAN_POINT('Ctrl Pts',(-2.44603200136559,-1.80297936806755,1.80297936806755));
#9545=CARTESIAN_POINT('Ctrl Pts',(-2.38353200136559,-2.549797875,1.0561608611351));
#9546=CARTESIAN_POINT('Ctrl Pts',(-2.3210320013656,-2.549797875,4.68390270913721E-16));
#9547=CARTESIAN_POINT('Ctrl Pts',(-2.25853200136559,-2.549797875,-1.0561608611351));
#9548=CARTESIAN_POINT('Ctrl Pts',(-2.1960320013656,-1.80297936806755,-1.80297936806755));
#9549=CARTESIAN_POINT('Ctrl Pts',(-2.13353200136559,-1.0561608611351,-2.549797875));
#9550=CARTESIAN_POINT('Ctrl Pts',(-2.07103200136559,0.,-2.549797875));
#9551=CARTESIAN_POINT('Ctrl Pts',(-2.00853200136559,1.0561608611351,-2.549797875));
#9552=CARTESIAN_POINT('Ctrl Pts',(-1.9460320013656,1.80297936806755,-1.80297936806755));
#9553=CARTESIAN_POINT('Ctrl Pts',(-1.8835320013656,2.549797875,-1.0561608611351));
#9554=CARTESIAN_POINT('Ctrl Pts',(-1.82103200136559,2.549797875,-1.56130090304574E-16));
#9555=CARTESIAN_POINT('Ctrl Pts',(-1.7585320013656,2.549797875,1.0561608611351));
#9556=CARTESIAN_POINT('Ctrl Pts',(-1.69603200136559,1.80297936806755,1.80297936806755));
#9557=CARTESIAN_POINT('Ctrl Pts',(-1.63353200136559,1.0561608611351,2.549797875));
#9558=CARTESIAN_POINT('Ctrl Pts',(-1.5710320013656,3.12260180609148E-16,
2.549797875));
#9559=CARTESIAN_POINT('Ctrl Pts',(-2.6960320013656,3.12260180609148E-16,
2.549797875));
#9560=CARTESIAN_POINT('Ctrl Pts',(-2.6335320013656,-1.0561608611351,2.549797875));
#9561=CARTESIAN_POINT('Ctrl Pts',(-2.5710320013656,-1.80297936806755,1.80297936806755));
#9562=CARTESIAN_POINT('Ctrl Pts',(-2.5085320013656,-2.549797875,1.0561608611351));
#9563=CARTESIAN_POINT('Ctrl Pts',(-2.44603200136559,-2.549797875,4.68390270913721E-16));
#9564=CARTESIAN_POINT('Ctrl Pts',(-2.38353200136559,-2.549797875,-1.0561608611351));
#9565=CARTESIAN_POINT('Ctrl Pts',(-2.3210320013656,-1.80297936806755,-1.80297936806755));
#9566=CARTESIAN_POINT('Ctrl Pts',(-2.25853200136559,-1.0561608611351,-2.549797875));
#9567=CARTESIAN_POINT('Ctrl Pts',(-2.1960320013656,0.,-2.549797875));
#9568=CARTESIAN_POINT('Ctrl Pts',(-2.13353200136559,1.0561608611351,-2.549797875));
#9569=CARTESIAN_POINT('Ctrl Pts',(-2.07103200136559,1.80297936806755,-1.80297936806755));
#9570=CARTESIAN_POINT('Ctrl Pts',(-2.00853200136559,2.549797875,-1.0561608611351));
#9571=CARTESIAN_POINT('Ctrl Pts',(-1.9460320013656,2.549797875,-1.56130090304574E-16));
#9572=CARTESIAN_POINT('Ctrl Pts',(-1.8835320013656,2.549797875,1.0561608611351));
#9573=CARTESIAN_POINT('Ctrl Pts',(-1.82103200136559,1.80297936806755,1.80297936806755));
#9574=CARTESIAN_POINT('Ctrl Pts',(-1.7585320013656,1.0561608611351,2.549797875));
#9575=CARTESIAN_POINT('Ctrl Pts',(-1.69603200136559,3.12260180609148E-16,
2.549797875));
#9576=CARTESIAN_POINT('Origin',(-4.1335320013656,6.79957634403871E-15,-6.66133814775094E-15));
#9577=CARTESIAN_POINT('',(-3.6960320013656,7.11183652464788E-15,2.549797875));
#9578=CARTESIAN_POINT('',(-3.57103200136559,7.11183652464788E-15,2.549797875));
#9579=CARTESIAN_POINT('',(-4.1335320013656,1.39114128686866E-14,2.54979787499999));
#9580=CARTESIAN_POINT('',(-4.,2.40346423367405,-0.851368827714594));
#9581=CARTESIAN_POINT('Ctrl Pts',(-4.,2.40346423367405,-0.851368827714594));
#9582=CARTESIAN_POINT('Ctrl Pts',(-3.97196675564161,2.549797875,-0.438260358551676));
#9583=CARTESIAN_POINT('Ctrl Pts',(-3.9460320013656,2.549797875,-1.56130090304574E-16));
#9584=CARTESIAN_POINT('Ctrl Pts',(-3.88353200136559,2.549797875,1.0561608611351));
#9585=CARTESIAN_POINT('Ctrl Pts',(-3.8210320013656,1.80297936806755,1.80297936806755));
#9586=CARTESIAN_POINT('Ctrl Pts',(-3.75853200136559,1.0561608611351,2.549797875));
#9587=CARTESIAN_POINT('Ctrl Pts',(-3.6960320013656,3.12260180609148E-16,
2.549797875));
#9588=CARTESIAN_POINT('',(-4.,1.09749718660243,-2.30151452933807));
#9589=CARTESIAN_POINT('Origin',(-4.,6.79957634403871E-15,-6.66133814775094E-15));
#9590=CARTESIAN_POINT('Ctrl Pts',(-4.,1.09749718660243,-2.30151452933807));
#9591=CARTESIAN_POINT('Ctrl Pts',(-3.97196675564161,1.49308249661042,-2.11287623952468));
#9592=CARTESIAN_POINT('Ctrl Pts',(-3.9460320013656,1.80297936806755,-1.80297936806755));
#9593=CARTESIAN_POINT('Ctrl Pts',(-3.88353200136559,2.549797875,-1.0561608611351));
#9594=CARTESIAN_POINT('Ctrl Pts',(-3.8210320013656,2.549797875,-1.56130090304574E-16));
#9595=CARTESIAN_POINT('Ctrl Pts',(-3.75853200136559,2.549797875,1.0561608611351));
#9596=CARTESIAN_POINT('Ctrl Pts',(-3.6960320013656,1.80297936806755,1.80297936806755));
#9597=CARTESIAN_POINT('Ctrl Pts',(-3.63353200136559,1.0561608611351,2.549797875));
#9598=CARTESIAN_POINT('Ctrl Pts',(-3.57103200136559,3.12260180609148E-16,
2.549797875));
#9599=CARTESIAN_POINT('Origin',(-3.508532,0.,0.));
#9600=CARTESIAN_POINT('',(-3.508532,0.,-2.008532));
#9601=CARTESIAN_POINT('',(-4.00000000000008,-3.06161699786848E-16,-2.50000000000008));
#9602=CARTESIAN_POINT('',(-3.508532,-2.45974228478503E-16,-2.008532));
#9603=CARTESIAN_POINT('',(-3.508532,2.008532,3.63558707729711E-8));
#9604=CARTESIAN_POINT('Origin',(-3.508532,0.,0.));
#9605=CARTESIAN_POINT('',(-4.,0.663411757904749,-2.41037027020201));
#9606=CARTESIAN_POINT('Ctrl Pts',(-3.50853200000001,2.00853200000001,3.6355872479677E-8));
#9607=CARTESIAN_POINT('Ctrl Pts',(-3.53382612947289,2.03382613204873,-0.142306019496749));
#9608=CARTESIAN_POINT('Ctrl Pts',(-3.57736045030338,2.06353600790935,-0.386343636106257));
#9609=CARTESIAN_POINT('Ctrl Pts',(-3.67936504533042,1.97724583342445,-0.952917190711209));
#9610=CARTESIAN_POINT('Ctrl Pts',(-3.7250839713689,1.88868644811177,-1.20522505423621));
#9611=CARTESIAN_POINT('Ctrl Pts',(-3.78543276629123,1.70131965479837,-1.52981386634904));
#9612=CARTESIAN_POINT('Ctrl Pts',(-3.8042150333194,1.63228546614519,-1.63220361975085));
#9613=CARTESIAN_POINT('Ctrl Pts',(-3.85459829755779,1.42567390080877,-1.88282757659245));
#9614=CARTESIAN_POINT('Ctrl Pts',(-3.8838183841557,1.29197929165672,-2.01166246391125));
#9615=CARTESIAN_POINT('Ctrl Pts',(-3.94240582504991,0.996071238886274,-2.23772216093148));
#9616=CARTESIAN_POINT('Ctrl Pts',(-3.97157997728534,0.834519750270115,-2.33379900101778));
#9617=CARTESIAN_POINT('Ctrl Pts',(-4.00000000000008,0.663411757904799,-2.41037027020209));
#9618=CARTESIAN_POINT('Origin',(-4.,0.,0.));
#9619=CARTESIAN_POINT('Origin',(0.,0.,0.));
#9620=CARTESIAN_POINT('',(-0.343792495187435,-1.84798906267329E-17,2.15620750481256));
#9621=CARTESIAN_POINT('',(2.39626859034904E-16,-3.06161699786838E-16,2.5));
#9622=CARTESIAN_POINT('',(0.,-3.06161699786838E-16,2.5));
#9623=CARTESIAN_POINT('',(-0.491468,1.99622053939136,0.222045835664713));
#9624=CARTESIAN_POINT('Ctrl Pts',(-0.343792495187436,2.27099480653155E-16,
2.15620750481256));
#9625=CARTESIAN_POINT('Ctrl Pts',(-0.346835563302273,0.068592189879008,
2.15316443669773));
#9626=CARTESIAN_POINT('Ctrl Pts',(-0.349953972956135,0.137232557864158,
2.14676612902208));
#9627=CARTESIAN_POINT('Ctrl Pts',(-0.365326801994469,0.467558433699237,
2.09956409034472));
#9628=CARTESIAN_POINT('Ctrl Pts',(-0.378214054572241,0.720278039460965,
2.01322828587724));
#9629=CARTESIAN_POINT('Ctrl Pts',(-0.397835304293012,1.06917445992625,1.8150899345924));
#9630=CARTESIAN_POINT('Ctrl Pts',(-0.404478939263286,1.18106791295702,1.73634110638149));
#9631=CARTESIAN_POINT('Ctrl Pts',(-0.422639367746322,1.46966390990759,1.4882674492164));
#9632=CARTESIAN_POINT('Ctrl Pts',(-0.43507971277735,1.65099064940197,1.27684962103764));
#9633=CARTESIAN_POINT('Ctrl Pts',(-0.457107777658471,1.84707317679396,0.883230819666249));
#9634=CARTESIAN_POINT('Ctrl Pts',(-0.4640029816804,1.8952762649122,0.756026772227834));
#9635=CARTESIAN_POINT('Ctrl Pts',(-0.477826971755898,1.96583127251109,0.493210297151591));
#9636=CARTESIAN_POINT('Ctrl Pts',(-0.484720391457909,1.98786166530542,0.358229176938792));
#9637=CARTESIAN_POINT('Ctrl Pts',(-0.491468,1.99622053939137,0.222045835664711));
#9638=CARTESIAN_POINT('',(-0.49146799999999,0.222045800910263,-1.99622054325721));
#9639=CARTESIAN_POINT('Origin',(-0.491468,0.,0.));
#9640=CARTESIAN_POINT('',(2.36346660700959E-16,2.46710998658661,-0.404188463571893));
#9641=CARTESIAN_POINT('Ctrl Pts',(-0.491467999999976,0.22204580091026,-1.99622054325724));
#9642=CARTESIAN_POINT('Ctrl Pts',(-0.448230267693132,0.459369200980115,
-2.0133267215389));
#9643=CARTESIAN_POINT('Ctrl Pts',(-0.404633819457699,0.697802895750879,
-1.98960723762313));
#9644=CARTESIAN_POINT('Ctrl Pts',(-0.297858721744298,1.27716376442399,-1.82918786458872));
#9645=CARTESIAN_POINT('Ctrl Pts',(-0.253226754599606,1.51258806051641,-1.66615397659853));
#9646=CARTESIAN_POINT('Ctrl Pts',(-0.195036445899189,1.81238247207411,-1.44449973647153));
#9647=CARTESIAN_POINT('Ctrl Pts',(-0.155671364837018,1.98548385608536,-1.26966634451936));
#9648=CARTESIAN_POINT('Ctrl Pts',(-0.0765988208212301,2.27597002415698,
-0.868392304059463));
#9649=CARTESIAN_POINT('Ctrl Pts',(-0.0373743863901998,2.39007414194648,
-0.643235206290509));
#9650=CARTESIAN_POINT('Ctrl Pts',(-6.67868538251071E-16,2.46710998658661,
-0.404188463571894));
#9651=CARTESIAN_POINT('Origin',(0.,0.,0.));
#9652=CARTESIAN_POINT('Origin',(0.,0.,0.));
#9653=CARTESIAN_POINT('',(-2.50853200000007,-4.84827408638443E-13,-2.008532));
#9654=CARTESIAN_POINT('',(-2.75853200273112,4.5044732021816E-13,-2.008532));
#9655=CARTESIAN_POINT('',(0.,-2.45974228478503E-16,-2.008532));
#9656=CARTESIAN_POINT('Ctrl Pts',(-2.75853200273112,9.01084762361393E-13,
-2.008532));
#9657=CARTESIAN_POINT('Ctrl Pts',(-2.77456055212585,-0.213362097700962,
-2.008532));
#9658=CARTESIAN_POINT('Ctrl Pts',(-2.79156461992547,-0.425632430784419,
-1.97454648813002));
#9659=CARTESIAN_POINT('Ctrl Pts',(-2.83007698894459,-0.876690264569696,
-1.82584321873764));
#9660=CARTESIAN_POINT('Ctrl Pts',(-2.85134459536468,-1.10626401391303,-1.69661658903667));
#9661=CARTESIAN_POINT('Ctrl Pts',(-2.8919216544136,-1.50521292752755,-1.35575932192851));
#9662=CARTESIAN_POINT('Ctrl Pts',(-2.9118599566143,-1.67003511935622,-1.1466282571683));
#9663=CARTESIAN_POINT('Ctrl Pts',(-2.95440287010154,-1.90822520426924,-0.678984970559192));
#9664=CARTESIAN_POINT('Ctrl Pts',(-2.97568935673053,-1.98024302784687,-0.425463236213872));
#9665=CARTESIAN_POINT('Ctrl Pts',(-3.0163093462195,-2.02340063934787,0.0973683756301305));
#9666=CARTESIAN_POINT('Ctrl Pts',(-3.03618042320102,-1.99319715537815,0.361686706262085));
#9667=CARTESIAN_POINT('Ctrl Pts',(-3.07869865966288,-1.83315117101439,0.86136985389795));
#9668=CARTESIAN_POINT('Ctrl Pts',(-3.10000450055328,-1.7057348138004,1.09220239618666));
#9669=CARTESIAN_POINT('Ctrl Pts',(-3.14066896724781,-1.36830702982799,1.49373536453641));
#9670=CARTESIAN_POINT('Ctrl Pts',(-3.16047214757596,-1.16095821365585,1.66003135284234));
#9671=CARTESIAN_POINT('Ctrl Pts',(-3.20296419129915,-0.695657166562376,
1.90224132737754));
#9672=CARTESIAN_POINT('Ctrl Pts',(-3.22428981667312,-0.442552167990885,
1.97652302286004));
#9673=CARTESIAN_POINT('Ctrl Pts',(-3.26500027165569,0.079646828549336,2.02411514822785));
#9674=CARTESIAN_POINT('Ctrl Pts',(-3.28473516831841,0.343737016683785,1.99630822223585));
#9675=CARTESIAN_POINT('Ctrl Pts',(-3.32719944636982,0.84464396057714,1.84095077849946));
#9676=CARTESIAN_POINT('Ctrl Pts',(-3.34854523630185,1.07682912175842,1.71551610930506));
#9677=CARTESIAN_POINT('Ctrl Pts',(-3.38930314393295,1.48115404399385,1.38182583248953));
#9678=CARTESIAN_POINT('Ctrl Pts',(-3.40896968143032,1.64904253759952,1.17640639382414));
#9679=CARTESIAN_POINT('Ctrl Pts',(-3.44364132718139,1.85048763662499,0.798320264684737));
#9680=CARTESIAN_POINT('Ctrl Pts',(-3.45715263173166,1.90998221265315,0.643109627718993));
#9681=CARTESIAN_POINT('Ctrl Pts',(-3.48354365253707,1.98881459742706,0.324462187400849));
#9682=CARTESIAN_POINT('Ctrl Pts',(-3.49632501857545,2.00853199705883,0.162491792763301));
#9683=CARTESIAN_POINT('Ctrl Pts',(-3.50853200000005,2.008532,3.63552882937102E-8));
#9684=CARTESIAN_POINT('Ctrl Pts',(-3.50853200000007,-9.84420878147318E-13,
-2.008532));
#9685=CARTESIAN_POINT('Ctrl Pts',(-3.49046402821612,0.24050962230436,-2.00853200000012));
#9686=CARTESIAN_POINT('Ctrl Pts',(-3.47118913480691,0.479191425417207,-1.96533300281851));
#9687=CARTESIAN_POINT('Ctrl Pts',(-3.43195318010694,0.931316582506389,-1.79595295990627));
#9688=CARTESIAN_POINT('Ctrl Pts',(-3.41231741129813,1.1408277657495,-1.67073258000721));
#9689=CARTESIAN_POINT('Ctrl Pts',(-3.37380973218154,1.51700588350948,-1.34140440174912));
#9690=CARTESIAN_POINT('Ctrl Pts',(-3.35418898308051,1.67650575064658,-1.13579659149845));
#9691=CARTESIAN_POINT('Ctrl Pts',(-3.31160830748131,1.91328256950635,-0.667065245134157));
#9692=CARTESIAN_POINT('Ctrl Pts',(-3.28982593566044,1.98498673948956,-0.406812675428285));
#9693=CARTESIAN_POINT('Ctrl Pts',(-3.24933193849708,2.02162373382201,0.117042732869852));
#9694=CARTESIAN_POINT('Ctrl Pts',(-3.22975941185735,1.98993503616935,0.37529971433039));
#9695=CARTESIAN_POINT('Ctrl Pts',(-3.18720029581631,1.82772911320931,0.874632349682423));
#9696=CARTESIAN_POINT('Ctrl Pts',(-3.16541623828598,1.69530469933909,1.10975620997746));
#9697=CARTESIAN_POINT('Ctrl Pts',(-3.12488147033888,1.35233179291034,1.50726584420255));
#9698=CARTESIAN_POINT('Ctrl Pts',(-3.10535792486904,1.14792370883617,1.66821748998151));
#9699=CARTESIAN_POINT('Ctrl Pts',(-3.06282169833356,0.681147963820842,1.9082871102709));
#9700=CARTESIAN_POINT('Ctrl Pts',(-3.04103617811804,0.421629789606673,1.98186544623294));
#9701=CARTESIAN_POINT('Ctrl Pts',(-3.00045894616575,-0.101698818431005,
2.02244912469178));
#9702=CARTESIAN_POINT('Ctrl Pts',(-2.98098493355571,-0.360143118773108,
1.99272777038104));
#9703=CARTESIAN_POINT('Ctrl Pts',(-2.93847298163481,-0.860460138050051,
1.83441405075633));
#9704=CARTESIAN_POINT('Ctrl Pts',(-2.91668626529548,-1.0964215950684,1.70392632940774));
#9705=CARTESIAN_POINT('Ctrl Pts',(-2.87606489189739,-1.49645967791858,1.36427444082656));
#9706=CARTESIAN_POINT('Ctrl Pts',(-2.85664073019463,-1.65900786950074,1.16118486715188));
#9707=CARTESIAN_POINT('Ctrl Pts',(-2.81415449127765,-1.90268273496045,0.69656786772297));
#9708=CARTESIAN_POINT('Ctrl Pts',(-2.79236689209776,-1.97831101929844,0.437871136045353));
#9709=CARTESIAN_POINT('Ctrl Pts',(-2.75169972683183,-2.02322266864599,-0.0848619041858379));
#9710=CARTESIAN_POINT('Ctrl Pts',(-2.73232547388737,-1.99565758636962,-0.343512247713487));
#9711=CARTESIAN_POINT('Ctrl Pts',(-2.6898664370209,-1.84160494767054,-0.84488989214959));
#9712=CARTESIAN_POINT('Ctrl Pts',(-2.66807831795509,-1.71324244732735,-1.08175031675541));
#9713=CARTESIAN_POINT('Ctrl Pts',(-2.62736374935824,-1.37723452127275,-1.48453833492761));
#9714=CARTESIAN_POINT('Ctrl Pts',(-2.6080391768759,-1.17558488172237,-1.64883138142115));
#9715=CARTESIAN_POINT('Ctrl Pts',(-2.56560887833205,-0.713336568558181,
-1.8964270329139));
#9716=CARTESIAN_POINT('Ctrl Pts',(-2.54382065462528,-0.455553842404719,
-1.97428199190002));
#9717=CARTESIAN_POINT('Ctrl Pts',(-2.51815002732461,-0.126787411536768,
-2.00553403794086));
#9718=CARTESIAN_POINT('Ctrl Pts',(-2.51329191108178,-0.0633609809763618,
-2.00853199999997));
#9719=CARTESIAN_POINT('Ctrl Pts',(-2.50853200000007,-9.69408843048408E-13,
-2.008532));
#9720=CARTESIAN_POINT('Origin',(0.,0.,0.));
#9721=CARTESIAN_POINT('',(-1.50853200000003,-1.87893736619935E-13,-2.008532));
#9722=CARTESIAN_POINT('',(-1.75853200273116,1.91028052360107E-13,-2.008532));
#9723=CARTESIAN_POINT('',(0.,-2.45974228478503E-16,-2.008532));
#9724=CARTESIAN_POINT('Ctrl Pts',(-1.75853200273116,3.82471831983366E-13,
-2.008532));
#9725=CARTESIAN_POINT('Ctrl Pts',(-1.77537323605212,-0.224180041546037,
-2.008532));
#9726=CARTESIAN_POINT('Ctrl Pts',(-1.79327970945474,-0.446997704203966,
-1.97100982574499));
#9727=CARTESIAN_POINT('Ctrl Pts',(-1.83325007951551,-0.912115609212472,
-1.80939550301654));
#9728=CARTESIAN_POINT('Ctrl Pts',(-1.85502063478529,-1.14493359087161,-1.67183812122849));
#9729=CARTESIAN_POINT('Ctrl Pts',(-1.89531797748143,-1.53563528603391,-1.32005941540903));
#9730=CARTESIAN_POINT('Ctrl Pts',(-1.9151454613833,-1.69232269859826,-1.11212547518953));
#9731=CARTESIAN_POINT('Ctrl Pts',(-1.95780947951013,-1.92268217297538,-0.639626573724209));
#9732=CARTESIAN_POINT('Ctrl Pts',(-1.97958232170033,-1.99072930021264,-0.377986059841389));
#9733=CARTESIAN_POINT('Ctrl Pts',(-2.02046371196938,-2.02008838063642,0.154040695600997));
#9734=CARTESIAN_POINT('Ctrl Pts',(-2.04083576575705,-1.98214662124489,0.419078454838985));
#9735=CARTESIAN_POINT('Ctrl Pts',(-2.08351416665944,-1.80704520927283,0.914657449761193));
#9736=CARTESIAN_POINT('Ctrl Pts',(-2.1046801365488,-1.67335278521896,1.14102848412408));
#9737=CARTESIAN_POINT('Ctrl Pts',(-2.14503284668744,-1.32396908043453,1.53345923821485));
#9738=CARTESIAN_POINT('Ctrl Pts',(-2.16534800272504,-1.11035708368627,1.69456239610697));
#9739=CARTESIAN_POINT('Ctrl Pts',(-2.20801059996808,-0.636915298361913,
1.9225998852347));
#9740=CARTESIAN_POINT('Ctrl Pts',(-2.22919202191717,-0.382435752508305,
1.98892893493238));
#9741=CARTESIAN_POINT('Ctrl Pts',(-2.26957817706242,0.141904562212205,2.02092959529444));
#9742=CARTESIAN_POINT('Ctrl Pts',(-2.28983454425305,0.406789812894553,1.98465498207741));
#9743=CARTESIAN_POINT('Ctrl Pts',(-2.33248025777436,0.903272599338705,1.81278597426953));
#9744=CARTESIAN_POINT('Ctrl Pts',(-2.35367774482194,1.13061657281339,1.68042958148138));
#9745=CARTESIAN_POINT('Ctrl Pts',(-2.39409890772545,1.52501936204394,1.33360695757695));
#9746=CARTESIAN_POINT('Ctrl Pts',(-2.41429469159831,1.68724808803654,1.12134842182099));
#9747=CARTESIAN_POINT('Ctrl Pts',(-2.45692237988489,1.91835911857486,0.649644425387381));
#9748=CARTESIAN_POINT('Ctrl Pts',(-2.47813653527762,1.98640587517699,0.395440649751718));
#9749=CARTESIAN_POINT('Ctrl Pts',(-2.51859428604895,2.02177771589593,-0.128456312865644));
#9750=CARTESIAN_POINT('Ctrl Pts',(-2.53872781259309,1.98734394944944,-0.393171494941496));
#9751=CARTESIAN_POINT('Ctrl Pts',(-2.58133627155539,1.81905137160877,-0.890639777624114));
#9752=CARTESIAN_POINT('Ctrl Pts',(-2.60256768385786,1.6881805612415,-1.11905069141494));
#9753=CARTESIAN_POINT('Ctrl Pts',(-2.6430636129712,1.34419532529303,-1.51562400658278));
#9754=CARTESIAN_POINT('Ctrl Pts',(-2.66313335395705,1.13342870882672,-1.67909113971857));
#9755=CARTESIAN_POINT('Ctrl Pts',(-2.70572131623673,0.663653961037752,-1.91358313320274));
#9756=CARTESIAN_POINT('Ctrl Pts',(-2.72697055406582,0.409767730895626,-1.98352393957922));
#9757=CARTESIAN_POINT('Ctrl Pts',(-2.75098176054802,0.0997356834155793,
-2.00667679103208));
#9758=CARTESIAN_POINT('Ctrl Pts',(-2.75478766083053,0.0498423545863755,
-2.008532));
#9759=CARTESIAN_POINT('Ctrl Pts',(-2.75853200273112,9.01140614664799E-13,
-2.008532));
#9760=CARTESIAN_POINT('Ctrl Pts',(-2.50853200000007,-9.69432867314879E-13,
-2.008532));
#9761=CARTESIAN_POINT('Ctrl Pts',(-2.49399315289905,0.193532105696083,-2.00853200000009));
#9762=CARTESIAN_POINT('Ctrl Pts',(-2.47863992207159,0.386323202437939,-1.98057159372929));
#9763=CARTESIAN_POINT('Ctrl Pts',(-2.44138171048376,0.827895436688843,-1.8492723066343));
#9764=CARTESIAN_POINT('Ctrl Pts',(-2.41959385185823,1.06571197843661,-1.72322644690499));
#9765=CARTESIAN_POINT('Ctrl Pts',(-2.37877986112267,1.47146879642677,-1.39119075688095));
#9766=CARTESIAN_POINT('Ctrl Pts',(-2.35955269820111,1.63765593032482,-1.1911029144753));
#9767=CARTESIAN_POINT('Ctrl Pts',(-2.31718465159873,1.88948442789464,-0.731436562757464));
#9768=CARTESIAN_POINT('Ctrl Pts',(-2.29539768390315,1.96973980952704,-0.474664843460665));
#9769=CARTESIAN_POINT('Ctrl Pts',(-2.25453181651249,2.02446596771235,0.0466478934158013));
#9770=CARTESIAN_POINT('Ctrl Pts',(-2.23535169477563,2.00178748462765,0.305768161170202));
#9771=CARTESIAN_POINT('Ctrl Pts',(-2.19301723102606,1.85737034409159,0.809478719638799));
#9772=CARTESIAN_POINT('Ctrl Pts',(-2.17123173724092,1.7338315431404,1.04830223984719));
#9773=CARTESIAN_POINT('Ctrl Pts',(-2.13031266638767,1.40609525397113,1.45723868926572));
#9774=CARTESIAN_POINT('Ctrl Pts',(-2.11117798753703,1.20768891749111,1.6254669535037));
#9775=CARTESIAN_POINT('Ctrl Pts',(-2.06887877944622,0.750816893465448,1.88182932523272));
#9776=CARTESIAN_POINT('Ctrl Pts',(-2.04709539994176,0.495156108327564,1.96465142723139));
#9777=CARTESIAN_POINT('Ctrl Pts',(-2.00612190301594,-0.0253221998097055,
2.02485091244375));
#9778=CARTESIAN_POINT('Ctrl Pts',(-1.98703068448704,-0.284706281507777,
2.00489648210646));
#9779=CARTESIAN_POINT('Ctrl Pts',(-1.9450715752669,-0.786052589074438,1.86683412031729));
#9780=CARTESIAN_POINT('Ctrl Pts',(-1.92360030332328,-1.02280145255032,1.74838464892588));
#9781=CARTESIAN_POINT('Ctrl Pts',(-1.88253079898025,-1.43667772949327,1.4277397507126));
#9782=CARTESIAN_POINT('Ctrl Pts',(-1.86325589841118,-1.6100205411952,1.22895066344172));
#9783=CARTESIAN_POINT('Ctrl Pts',(-1.82103392456302,-1.87139489634744,0.775182765209177));
#9784=CARTESIAN_POINT('Ctrl Pts',(-1.79954171907214,-1.95655067049019,0.524364546407468));
#9785=CARTESIAN_POINT('Ctrl Pts',(-1.75841678561011,-2.0254198564022,0.00546151673586223));
#9786=CARTESIAN_POINT('Ctrl Pts',(-1.73920026493478,-2.00898958408763,-0.257521591994173));
#9787=CARTESIAN_POINT('Ctrl Pts',(-1.69702003124529,-1.87603869397377,-0.763928612096199));
#9788=CARTESIAN_POINT('Ctrl Pts',(-1.67550710708127,-1.76024404664785,-1.00233158820248));
#9789=CARTESIAN_POINT('Ctrl Pts',(-1.63432606389763,-1.4445089394228,-1.41972630295501));
#9790=CARTESIAN_POINT('Ctrl Pts',(-1.61516486190513,-1.24817429840401,-1.59508307320836));
#9791=CARTESIAN_POINT('Ctrl Pts',(-1.57302815681787,-0.797799720262673,
-1.86190938718852));
#9792=CARTESIAN_POINT('Ctrl Pts',(-1.55149481751584,-0.547724619970668,
-1.95018110533127));
#9793=CARTESIAN_POINT('Ctrl Pts',(-1.52318811370744,-0.192237777317641,
-2.00163867517231));
#9794=CARTESIAN_POINT('Ctrl Pts',(-1.51575009246435,-0.0960827653000358,
-2.00853199999998));
#9795=CARTESIAN_POINT('Ctrl Pts',(-1.50853200000003,-3.75541499011392E-13,
-2.008532));
#9796=CARTESIAN_POINT('Origin',(0.,0.,0.));
#9797=CARTESIAN_POINT('',(-0.508531999999968,2.08048577268714E-13,-2.008532));
#9798=CARTESIAN_POINT('',(-0.758532002731178,6.47213330337261E-14,-2.008532));
#9799=CARTESIAN_POINT('',(0.,-2.45974228478503E-16,-2.008532));
#9800=CARTESIAN_POINT('Ctrl Pts',(-0.508531999999968,4.16343128765906E-13,
-2.008532));
#9801=CARTESIAN_POINT('Ctrl Pts',(-0.50296733755124,0.074073331517712,-2.008532));
#9802=CARTESIAN_POINT('Ctrl Pts',(-0.497271803520675,0.148191934104109,
-2.00443553786825));
#9803=CARTESIAN_POINT('Ctrl Pts',(-0.49146799999999,0.222045800910263,-1.99622054325721));
#9804=CARTESIAN_POINT('Ctrl Pts',(-0.491467999999934,1.99622053939127,0.222045835665548));
#9805=CARTESIAN_POINT('Ctrl Pts',(-0.503500023483089,2.01325127151279,0.068937369749291));
#9806=CARTESIAN_POINT('Ctrl Pts',(-0.514833549485698,2.01261300279072,-0.085572684581587));
#9807=CARTESIAN_POINT('Ctrl Pts',(-0.539214417763003,1.9756272638048,-0.394795670738753));
#9808=CARTESIAN_POINT('Ctrl Pts',(-0.55189707065267,1.93863972224196,-0.548298530217973));
#9809=CARTESIAN_POINT('Ctrl Pts',(-0.586474880195251,1.79119618574373,-0.947503749599346));
#9810=CARTESIAN_POINT('Ctrl Pts',(-0.608223847068728,1.64877810702651,-1.17802099334014));
#9811=CARTESIAN_POINT('Ctrl Pts',(-0.648285515458815,1.28865128670949,-1.56212763622119));
#9812=CARTESIAN_POINT('Ctrl Pts',(-0.668456402771949,1.07733276611845,-1.7147277761548));
#9813=CARTESIAN_POINT('Ctrl Pts',(-0.711234900865904,0.599410782925871,
-1.9356737599134));
#9814=CARTESIAN_POINT('Ctrl Pts',(-0.732985768951428,0.335837238716916,
-1.99834796804225));
#9815=CARTESIAN_POINT('Ctrl Pts',(-0.755130222334065,0.0451250070225805,
-2.00815204740256));
#9816=CARTESIAN_POINT('Ctrl Pts',(-0.756837522219823,0.0225558724944502,
-2.008532));
#9817=CARTESIAN_POINT('Ctrl Pts',(-0.758532002731178,1.29688640295931E-13,
-2.008532));
#9818=CARTESIAN_POINT('Origin',(0.,0.,0.));
#9819=CARTESIAN_POINT('Ctrl Pts',(-0.758532002731179,1.29340982368831E-13,
-2.008532));
#9820=CARTESIAN_POINT('Ctrl Pts',(-0.776206629942389,-0.235273663573603,
-2.008532));
#9821=CARTESIAN_POINT('Ctrl Pts',(-0.795044682083602,-0.468914196920289,
-1.96720085563323));
#9822=CARTESIAN_POINT('Ctrl Pts',(-0.835979030048088,-0.942081937442259,
-1.7940416675059));
#9823=CARTESIAN_POINT('Ctrl Pts',(-0.857731872939479,-1.17295963346949,
-1.65236923589102));
#9824=CARTESIAN_POINT('Ctrl Pts',(-0.897830394354453,-1.55808762843327,
-1.29352384994752));
#9825=CARTESIAN_POINT('Ctrl Pts',(-0.917945023665489,-1.7113181533755,-1.08272761527968));
#9826=CARTESIAN_POINT('Ctrl Pts',(-0.960706386238093,-1.93372256231143,
-0.605637828996343));
#9827=CARTESIAN_POINT('Ctrl Pts',(-0.982461274020495,-1.99722972218349,
-0.342355796987144));
#9828=CARTESIAN_POINT('Ctrl Pts',(-1.0225799633235,-2.01670908902974,0.183610668098889));
#9829=CARTESIAN_POINT('Ctrl Pts',(-1.04266419617014,-1.97645171555318,0.441058478084166));
#9830=CARTESIAN_POINT('Ctrl Pts',(-1.08541606380662,-1.79725151794042,0.935917643954678));
#9831=CARTESIAN_POINT('Ctrl Pts',(-1.10717306177851,-1.65642642852138,1.16720163046321));
#9832=CARTESIAN_POINT('Ctrl Pts',(-1.14731315213468,-1.29903685763934,1.55348598370563));
#9833=CARTESIAN_POINT('Ctrl Pts',(-1.16736543584026,-1.08883275610851,1.70743133606404));
#9834=CARTESIAN_POINT('Ctrl Pts',(-1.21010713618721,-0.612688535434477,
1.93148666696733));
#9835=CARTESIAN_POINT('Ctrl Pts',(-1.2318663034081,-0.349740010443477,1.9959365102324));
#9836=CARTESIAN_POINT('Ctrl Pts',(-1.2720290820139,0.175999334796381,2.01738106929987));
#9837=CARTESIAN_POINT('Ctrl Pts',(-1.29204784227751,0.433539482549909,1.97810671882581));
#9838=CARTESIAN_POINT('Ctrl Pts',(-1.3347786597579,0.928927240966364,1.8008591350999));
#9839=CARTESIAN_POINT('Ctrl Pts',(-1.35654004741073,1.16066745678154,1.66099441162635));
#9840=CARTESIAN_POINT('Ctrl Pts',(-1.3967268548385,1.54825693866292,1.30525437627347));
#9841=CARTESIAN_POINT('Ctrl Pts',(-1.41671050468876,1.7030105400602,1.09571963930088));
#9842=CARTESIAN_POINT('Ctrl Pts',(-1.45942967847865,1.92892885105761,0.620646949789437));
#9843=CARTESIAN_POINT('Ctrl Pts',(-1.4811933280373,1.99444217192984,0.358079265549406));
#9844=CARTESIAN_POINT('Ctrl Pts',(-1.52140555706854,2.01810610587264,-0.16739903787763));
#9845=CARTESIAN_POINT('Ctrl Pts',(-1.54135250729902,1.97994137375992,-0.425043553993443));
#9846=CARTESIAN_POINT('Ctrl Pts',(-1.58405922934413,1.80489703799285,-0.921023184121574));
#9847=CARTESIAN_POINT('Ctrl Pts',(-1.60582517053885,1.66611752328278,-1.15327352204698));
#9848=CARTESIAN_POINT('Ctrl Pts',(-1.64606426442597,1.31224090848214,-1.54233086287674));
#9849=CARTESIAN_POINT('Ctrl Pts',(-1.66597293560513,1.10346035458751,-1.69799538218072));
#9850=CARTESIAN_POINT('Ctrl Pts',(-1.70866634870659,0.629598297633439,-1.92600856004427));
#9851=CARTESIAN_POINT('Ctrl Pts',(-1.73043459728279,0.367464563231961,-1.99271732488473));
#9852=CARTESIAN_POINT('Ctrl Pts',(-1.75350189558004,0.0666147617554255,
-2.00770416246007));
#9853=CARTESIAN_POINT('Ctrl Pts',(-1.75603081447768,0.033294265087432,-2.008532));
#9854=CARTESIAN_POINT('Ctrl Pts',(-1.75853200273116,3.82302078948693E-13,
-2.008532));
#9855=CARTESIAN_POINT('Ctrl Pts',(-1.50853200000003,-3.75845188305135E-13,
-2.008532));
#9856=CARTESIAN_POINT('Ctrl Pts',(-1.4962584313927,0.163378124859691,-2.00853200000003));
#9857=CARTESIAN_POINT('Ctrl Pts',(-1.48338752376592,0.326453885797803,-1.98860563634782));
#9858=CARTESIAN_POINT('Ctrl Pts',(-1.44905636215842,0.740690958538574,-1.88537860842314));
#9859=CARTESIAN_POINT('Ctrl Pts',(-1.42750299973453,0.980791387042714,-1.77238242907389));
#9860=CARTESIAN_POINT('Ctrl Pts',(-1.38620827425788,1.40183226807111,-1.46179659354929));
#9861=CARTESIAN_POINT('Ctrl Pts',(-1.36714693221582,1.57928024643194,-1.268012642573));
#9862=CARTESIAN_POINT('Ctrl Pts',(-1.32510251806025,1.85175170782269,-0.821204880631625));
#9863=CARTESIAN_POINT('Ctrl Pts',(-1.30352961156712,1.94325916583521,-0.57194337379661));
#9864=CARTESIAN_POINT('Ctrl Pts',(-1.26217761857935,2.02455466379949,-0.0551650156779208));
#9865=CARTESIAN_POINT('Ctrl Pts',(-1.24316007249524,2.01468227469715,0.207169081980398));
#9866=CARTESIAN_POINT('Ctrl Pts',(-1.2011643193693,1.89474571919842,0.716511125263879));
#9867=CARTESIAN_POINT('Ctrl Pts',(-1.17957243215547,1.78467224709688,0.958334996833248));
#9868=CARTESIAN_POINT('Ctrl Pts',(-1.13816309807723,1.4794374337588,1.38311794236977));
#9869=CARTESIAN_POINT('Ctrl Pts',(-1.11918480959087,1.2882791099408,1.56271755609484));
#9870=CARTESIAN_POINT('Ctrl Pts',(-1.07723930261779,0.845185758698867,1.84097786631538));
#9871=CARTESIAN_POINT('Ctrl Pts',(-1.05562907829457,0.596805733715434,1.93581267466358));
#9872=CARTESIAN_POINT('Ctrl Pts',(-1.01416249047248,0.0812001570578579,
2.02362219580507));
#9873=CARTESIAN_POINT('Ctrl Pts',(-0.99521862998263,-0.180794988375118,
2.01716443761624));
#9874=CARTESIAN_POINT('Ctrl Pts',(-0.953324866943538,-0.691596166203094,
1.90402815017389));
#9875=CARTESIAN_POINT('Ctrl Pts',(-0.931697024099726,-0.93515080245912,
1.79697762511782));
#9876=CARTESIAN_POINT('Ctrl Pts',(-0.890173431001628,-1.36373603292118,
1.49725045325215));
#9877=CARTESIAN_POINT('Ctrl Pts',(-0.871258921075412,-1.54552869401676,
1.30876853444956));
#9878=CARTESIAN_POINT('Ctrl Pts',(-0.829418297971695,-1.8296663418148,0.869505805091247));
#9879=CARTESIAN_POINT('Ctrl Pts',(-0.807773623713855,-1.92788820551147,
0.622070168229358));
#9880=CARTESIAN_POINT('Ctrl Pts',(-0.766193433292469,-2.0223340702211,0.10770124781425));
#9881=CARTESIAN_POINT('Ctrl Pts',(-0.747302997047551,-2.0193398374198,-0.153950268255605));
#9882=CARTESIAN_POINT('Ctrl Pts',(-0.705516794228873,-1.9131155891858,-0.666182731595407));
#9883=CARTESIAN_POINT('Ctrl Pts',(-0.68385613666116,-1.80916028141189,-0.911456258058694));
#9884=CARTESIAN_POINT('Ctrl Pts',(-0.642219912899481,-1.51504612288649,
-1.34386574423529));
#9885=CARTESIAN_POINT('Ctrl Pts',(-0.623348126422726,-1.32926520574239,
-1.527872263121));
#9886=CARTESIAN_POINT('Ctrl Pts',(-0.583787298578959,-0.916549650383403,
-1.80283579070201));
#9887=CARTESIAN_POINT('Ctrl Pts',(-0.564384926046246,-0.697799062386865,
-1.89824973210959));
#9888=CARTESIAN_POINT('Ctrl Pts',(-0.532702841586254,-0.314104129907558,
-1.99007990973763));
#9889=CARTESIAN_POINT('Ctrl Pts',(-0.52034291965406,-0.157219629244434,
-2.008532));
#9890=CARTESIAN_POINT('Ctrl Pts',(-0.508531999999968,4.18345913466567E-13,
-2.008532));
#9891=CARTESIAN_POINT('Origin',(-2.93767550469109,0.,0.));
#9892=CARTESIAN_POINT('',(-3.19240120012393,-2.30940107675851,-4.));
#9893=CARTESIAN_POINT('',(-3.19240120012393,2.30940107675851,-4.));
#9894=CARTESIAN_POINT('Ctrl Pts',(-3.19240120011886,-2.30940107677608,-4.));
#9895=CARTESIAN_POINT('Ctrl Pts',(-3.8590678667944,2.22044604925031E-16,
-4.));
#9896=CARTESIAN_POINT('Ctrl Pts',(-3.19240120011886,2.30940107677608,-4.));
#9897=CARTESIAN_POINT('',(-3.19240120012393,-4.61880215351701,0.));
#9898=CARTESIAN_POINT('Ctrl Pts',(-3.19240120011885,-4.6188021535258,1.52242598350499E-11));
#9899=CARTESIAN_POINT('Ctrl Pts',(-3.8590678667944,-3.46410161513776,-2.));
#9900=CARTESIAN_POINT('Ctrl Pts',(-3.19240120011886,-2.30940107674972,-4.00000000001522));
#9901=CARTESIAN_POINT('',(-3.19240120012393,-2.30940107675851,4.));
#9902=CARTESIAN_POINT('Ctrl Pts',(-3.19240120011886,-2.30940107674972,4.00000000001521));
#9903=CARTESIAN_POINT('Ctrl Pts',(-3.8590678667944,-3.46410161513776,2.));
#9904=CARTESIAN_POINT('Ctrl Pts',(-3.19240120011886,-4.61880215352579,-1.52191983380731E-11));
#9905=CARTESIAN_POINT('',(-3.54966679003209,3.14368002532301E-16,4.));
#9906=CARTESIAN_POINT('Ctrl Pts',(-3.19240120011886,-2.30940107677608,4.));
#9907=CARTESIAN_POINT('Ctrl Pts',(-3.54966679003209,-1.07179676973155,4.));
#9908=CARTESIAN_POINT('Ctrl Pts',(-3.54966679003209,1.11859472472354E-15,
4.));
#9909=CARTESIAN_POINT('',(-4.,-3.94336269325448E-16,3.22));
#9910=CARTESIAN_POINT('',(-2.93767550469109,-6.19671280368561E-16,5.06));
#9911=CARTESIAN_POINT('Origin',(-4.,0.,0.));
#9912=CARTESIAN_POINT('',(-3.19240120012393,2.30940107675851,4.));
#9913=CARTESIAN_POINT('Ctrl Pts',(-3.54966679003209,1.11859472472354E-15,
4.));
#9914=CARTESIAN_POINT('Ctrl Pts',(-3.54966679003209,1.07179676973155,4.));
#9915=CARTESIAN_POINT('Ctrl Pts',(-3.19240120011886,2.30940107677607,4.));
#9916=CARTESIAN_POINT('',(-3.19240120012393,4.61880215351701,0.));
#9917=CARTESIAN_POINT('Ctrl Pts',(-3.19240120011885,4.6188021535258,-1.52242598350499E-11));
#9918=CARTESIAN_POINT('Ctrl Pts',(-3.8590678667944,3.46410161513776,2.));
#9919=CARTESIAN_POINT('Ctrl Pts',(-3.19240120011886,2.30940107674972,4.00000000001522));
#9920=CARTESIAN_POINT('Ctrl Pts',(-3.19240120011886,2.30940107674972,-4.00000000001521));
#9921=CARTESIAN_POINT('Ctrl Pts',(-3.8590678667944,3.46410161513776,-2.));
#9922=CARTESIAN_POINT('Ctrl Pts',(-3.19240120011886,4.61880215352579,1.52191983380731E-11));
#9923=CARTESIAN_POINT('Origin',(0.,0.,0.));
#9924=CARTESIAN_POINT('',(1.17539427474239E-16,0.663411757905302,-2.41037027020186));
#9925=CARTESIAN_POINT('Origin',(0.,0.,0.));
#9926=CARTESIAN_POINT('Ctrl Pts',(-1.82145964977565E-16,0.663411757905292,
-2.41037027020186));
#9927=CARTESIAN_POINT('Ctrl Pts',(-0.0068932752031904,0.499867287283901,
-2.44823338935451));
#9928=CARTESIAN_POINT('Ctrl Pts',(-0.0137115664211188,0.33294396450463,
-2.46959882520677));
#9929=CARTESIAN_POINT('Ctrl Pts',(-0.0270997986546331,-0.00565733357005639,
-2.47877910626091));
#9930=CARTESIAN_POINT('Ctrl Pts',(-0.0336564761924616,-0.177008197745316,
-2.46598363045078));
#9931=CARTESIAN_POINT('Ctrl Pts',(-0.0536637583285811,-0.659952657991195,
-2.37710123135134));
#9932=CARTESIAN_POINT('Ctrl Pts',(-0.0672921528648265,-0.959245802836347,
-2.25820164274285));
#9933=CARTESIAN_POINT('Ctrl Pts',(-0.0927875713568389,-1.46471243278332,
-1.93113485588623));
#9934=CARTESIAN_POINT('Ctrl Pts',(-0.105075936490514,-1.70142949321577,
-1.71908597546532));
#9935=CARTESIAN_POINT('Ctrl Pts',(-0.132290467527035,-2.07148587907461,
-1.18757222236683));
#9936=CARTESIAN_POINT('Ctrl Pts',(-0.145927106519498,-2.19635742991887,
-0.901652475941354));
#9937=CARTESIAN_POINT('Ctrl Pts',(-0.171531588164497,-2.32125889322368,
-0.330603170846493));
#9938=CARTESIAN_POINT('Ctrl Pts',(-0.183808945617099,-2.33860361927158,
-0.0247236227682734));
#9939=CARTESIAN_POINT('Ctrl Pts',(-0.210295427797897,-2.2342235021799,0.576950904578398));
#9940=CARTESIAN_POINT('Ctrl Pts',(-0.223339016646017,-2.13237831290703,
0.84734778897084));
#9941=CARTESIAN_POINT('Ctrl Pts',(-0.243011417696767,-1.90645192751628,
1.21693862929627));
#9942=CARTESIAN_POINT('Ctrl Pts',(-0.24962020758457,-1.81794099851076,1.33446859700807));
#9943=CARTESIAN_POINT('Ctrl Pts',(-0.262569893827658,-1.61882738726217,
1.55154278536559));
#9944=CARTESIAN_POINT('Ctrl Pts',(-0.268850102427555,-1.50744739092849,
1.65165556226842));
#9945=CARTESIAN_POINT('Ctrl Pts',(-0.28784942229089,-1.16344806195362,1.90152272333394));
#9946=CARTESIAN_POINT('Ctrl Pts',(-0.300818689630185,-0.911979820987807,
2.02001175976281));
#9947=CARTESIAN_POINT('Ctrl Pts',(-0.320467201912672,-0.508066949584239,
2.12420208011994));
#9948=CARTESIAN_POINT('Ctrl Pts',(-0.32709177611566,-0.367859794683295,
2.14621003927891));
#9949=CARTESIAN_POINT('Ctrl Pts',(-0.337013615803521,-0.151496210248655,
2.15897970641058));
#9950=CARTESIAN_POINT('Ctrl Pts',(-0.340430365784306,-0.0757839817297517,
2.15956963421569));
#9951=CARTESIAN_POINT('Ctrl Pts',(-0.343792495187436,2.27099480653155E-16,
2.15620750481256));
#9952=CARTESIAN_POINT('Origin',(-3.508532,0.,0.));
#9953=CARTESIAN_POINT('',(-4.,2.46710998658661,-0.40418846357189));
#9954=CARTESIAN_POINT('Origin',(-4.,0.,0.));
#9955=CARTESIAN_POINT('Ctrl Pts',(-3.50853200000446,-9.37083836906508E-11,
-2.00853200000446));
#9956=CARTESIAN_POINT('Ctrl Pts',(-3.51292702417713,-0.0922810368142426,
-2.01292702417282));
#9957=CARTESIAN_POINT('Ctrl Pts',(-3.51857752432441,-0.208898649734097,
-2.01229229041598));
#9958=CARTESIAN_POINT('Ctrl Pts',(-3.53087885357248,-0.454106642669512,
-1.9825908865936));
#9959=CARTESIAN_POINT('Ctrl Pts',(-3.53650469184044,-0.563552638557295,
-1.9601450116639));
#9960=CARTESIAN_POINT('Ctrl Pts',(-3.55356981611893,-0.887604345263331,
-1.86554842964995));
#9961=CARTESIAN_POINT('Ctrl Pts',(-3.56492765125652,-1.09259900510742,-1.76667555549241));
#9962=CARTESIAN_POINT('Ctrl Pts',(-3.58247411882797,-1.39111902687923,-1.55591193265632));
#9963=CARTESIAN_POINT('Ctrl Pts',(-3.58874370607916,-1.49596069762447,-1.46420141740028));
#9964=CARTESIAN_POINT('Ctrl Pts',(-3.60164700981519,-1.68459789727543,-1.26406206035305));
#9965=CARTESIAN_POINT('Ctrl Pts',(-3.60824813690499,-1.76884843111482,-1.15528455891842));
#9966=CARTESIAN_POINT('Ctrl Pts',(-3.62792724143012,-1.98494271219238,-0.812282569527967));
#9967=CARTESIAN_POINT('Ctrl Pts',(-3.64099804154009,-2.08364449732469,-0.560403869526387));
#9968=CARTESIAN_POINT('Ctrl Pts',(-3.66807436475461,-2.19066070805393,0.0121812493841459));
#9969=CARTESIAN_POINT('Ctrl Pts',(-3.68062554807944,-2.17463256315328,0.305991508728111));
#9970=CARTESIAN_POINT('Ctrl Pts',(-3.70581838685037,-2.06141327516712,0.832935131054126));
#9971=CARTESIAN_POINT('Ctrl Pts',(-3.71894428739146,-1.95164994292461,1.09195784432159));
#9972=CARTESIAN_POINT('Ctrl Pts',(-3.73813174295214,-1.71442518947555,1.44627404668417));
#9973=CARTESIAN_POINT('Ctrl Pts',(-3.74436525939159,-1.6207689605633,1.55946508773479));
#9974=CARTESIAN_POINT('Ctrl Pts',(-3.76368926437764,-1.30374829832282,1.87462298805652));
#9975=CARTESIAN_POINT('Ctrl Pts',(-3.77733071684782,-1.05165672040478,2.04203466813512));
#9976=CARTESIAN_POINT('Ctrl Pts',(-3.79751331327142,-0.637746828063753,
2.21215772464066));
#9977=CARTESIAN_POINT('Ctrl Pts',(-3.80410247062574,-0.495924536937652,
2.25493873023327));
#9978=CARTESIAN_POINT('Ctrl Pts',(-3.82519226905413,-0.0202166467251451,
2.34938256657904));
#9979=CARTESIAN_POINT('Ctrl Pts',(-3.83747842364639,0.289777401984434,2.33503990053325));
#9980=CARTESIAN_POINT('Ctrl Pts',(-3.86266234370501,0.857667212957973,2.2230575522556));
#9981=CARTESIAN_POINT('Ctrl Pts',(-3.87627217552642,1.1463214551877,2.10429183070078));
#9982=CARTESIAN_POINT('Ctrl Pts',(-3.90401447671096,1.69531375267038,1.73991032599821));
#9983=CARTESIAN_POINT('Ctrl Pts',(-3.91630521053648,1.91239288512789,1.50297344723526));
#9984=CARTESIAN_POINT('Ctrl Pts',(-3.94007316637035,2.22828134319281,1.03459998543546));
#9985=CARTESIAN_POINT('Ctrl Pts',(-3.95225872728684,2.34532113430431,0.771188063445417));
#9986=CARTESIAN_POINT('Ctrl Pts',(-3.97957344612241,2.50469052679756,0.127998548371377));
#9987=CARTESIAN_POINT('Ctrl Pts',(-3.9911790709379,2.49377286047805,-0.186882496097888));
#9988=CARTESIAN_POINT('Ctrl Pts',(-3.99999999999735,2.46710998659464,-0.404188463506497));
#9989=CARTESIAN_POINT('Origin',(0.,5.06,0.));
#9990=CARTESIAN_POINT('',(0.,4.61880215351701,0.));
#9991=CARTESIAN_POINT('',(0.,2.30940107675851,4.));
#9992=CARTESIAN_POINT('',(0.,4.61880215351701,0.));
#9993=CARTESIAN_POINT('',(0.,-2.30940107675851,4.));
#9994=CARTESIAN_POINT('',(0.,2.30940107675851,4.));
#9995=CARTESIAN_POINT('',(0.,-4.61880215351701,0.));
#9996=CARTESIAN_POINT('',(0.,-2.30940107675851,4.));
#9997=CARTESIAN_POINT('',(0.,-2.30940107675851,-4.));
#9998=CARTESIAN_POINT('',(0.,-4.61880215351701,0.));
#9999=CARTESIAN_POINT('',(0.,2.30940107675851,-4.));
#10000=CARTESIAN_POINT('',(0.,-2.30940107675851,-4.));
#10001=CARTESIAN_POINT('',(0.,2.30940107675851,-4.));
#10002=CARTESIAN_POINT('Origin',(0.000123745270384153,-0.0786025494032175,
-0.269984759888047));
#10003=CARTESIAN_POINT('Origin',(-4.52827338442856E-5,0.270013278081845,
0.0783217498640101));
#10004=CARTESIAN_POINT('Origin',(-4.,0.,0.));
#10005=CARTESIAN_POINT('Origin',(-3.99996492800005,-0.0784507930919776,
-0.270006358878946));
#10006=CARTESIAN_POINT('Origin',(-4.00005184704125,0.270010503487591,0.0783328141479592));
#10007=CARTESIAN_POINT('Origin',(-4.,4.61880215351701,0.));
#10008=CARTESIAN_POINT('',(-4.,2.30940107675851,4.));
#10009=CARTESIAN_POINT('',(-4.,4.61880215351701,0.));
#10010=CARTESIAN_POINT('Origin',(-4.,2.30940107675851,-4.));
#10011=CARTESIAN_POINT('',(-4.,2.30940107675851,-4.));
#10012=CARTESIAN_POINT('Origin',(-4.,-2.30940107675851,-4.));
#10013=CARTESIAN_POINT('',(-4.,-2.30940107675851,-4.));
#10014=CARTESIAN_POINT('Origin',(-4.,-4.61880215351701,0.));
#10015=CARTESIAN_POINT('',(-4.,-4.61880215351701,0.));
#10016=CARTESIAN_POINT('Origin',(-4.,-2.30940107675851,4.));
#10017=CARTESIAN_POINT('',(-4.,-2.30940107675851,4.));
#10018=CARTESIAN_POINT('Origin',(-4.,2.30940107675851,4.));
#10019=CARTESIAN_POINT('Origin',(-4.1335320013656,6.79957634403871E-15,
-6.66133814775094E-15));
#10020=CARTESIAN_POINT('Ctrl Pts',(-3.57103200136559,3.12260180609148E-16,
2.549797875));
#10021=CARTESIAN_POINT('Ctrl Pts',(-3.50853200136559,-1.0561608611351,2.549797875));
#10022=CARTESIAN_POINT('Ctrl Pts',(-3.4460320013656,-1.80297936806755,1.80297936806755));
#10023=CARTESIAN_POINT('Ctrl Pts',(-3.3835320013656,-2.549797875,1.0561608611351));
#10024=CARTESIAN_POINT('Ctrl Pts',(-3.3210320013656,-2.549797875,4.68390270913721E-16));
#10025=CARTESIAN_POINT('Ctrl Pts',(-3.2585320013656,-2.549797875,-1.0561608611351));
#10026=CARTESIAN_POINT('Ctrl Pts',(-3.1960320013656,-1.80297936806755,-1.80297936806755));
#10027=CARTESIAN_POINT('Ctrl Pts',(-3.13353200136559,-1.0561608611351,-2.549797875));
#10028=CARTESIAN_POINT('Ctrl Pts',(-3.07103200136559,0.,-2.549797875));
#10029=CARTESIAN_POINT('Ctrl Pts',(-3.00853200136559,1.0561608611351,-2.549797875));
#10030=CARTESIAN_POINT('Ctrl Pts',(-2.94603200136559,1.80297936806755,-1.80297936806755));
#10031=CARTESIAN_POINT('Ctrl Pts',(-2.88353200136559,2.549797875,-1.0561608611351));
#10032=CARTESIAN_POINT('Ctrl Pts',(-2.82103200136559,2.549797875,-1.56130090304574E-16));
#10033=CARTESIAN_POINT('Ctrl Pts',(-2.75853200136559,2.549797875,1.0561608611351));
#10034=CARTESIAN_POINT('Ctrl Pts',(-2.6960320013656,1.80297936806755,1.80297936806755));
#10035=CARTESIAN_POINT('Ctrl Pts',(-2.6335320013656,1.0561608611351,2.549797875));
#10036=CARTESIAN_POINT('Ctrl Pts',(-2.5710320013656,3.12260180609148E-16,
2.549797875));
#10037=CARTESIAN_POINT('Ctrl Pts',(-3.6960320013656,3.12260180609148E-16,
2.549797875));
#10038=CARTESIAN_POINT('Ctrl Pts',(-3.63353200136559,-1.0561608611351,2.549797875));
#10039=CARTESIAN_POINT('Ctrl Pts',(-3.57103200136559,-1.80297936806755,
1.80297936806755));
#10040=CARTESIAN_POINT('Ctrl Pts',(-3.50853200136559,-2.549797875,1.0561608611351));
#10041=CARTESIAN_POINT('Ctrl Pts',(-3.4460320013656,-2.549797875,4.68390270913721E-16));
#10042=CARTESIAN_POINT('Ctrl Pts',(-3.3835320013656,-2.549797875,-1.0561608611351));
#10043=CARTESIAN_POINT('Ctrl Pts',(-3.3210320013656,-1.80297936806755,-1.80297936806755));
#10044=CARTESIAN_POINT('Ctrl Pts',(-3.2585320013656,-1.0561608611351,-2.549797875));
#10045=CARTESIAN_POINT('Ctrl Pts',(-3.1960320013656,0.,-2.549797875));
#10046=CARTESIAN_POINT('Ctrl Pts',(-3.13353200136559,1.0561608611351,-2.549797875));
#10047=CARTESIAN_POINT('Ctrl Pts',(-3.07103200136559,1.80297936806755,-1.80297936806755));
#10048=CARTESIAN_POINT('Ctrl Pts',(-3.00853200136559,2.549797875,-1.0561608611351));
#10049=CARTESIAN_POINT('Ctrl Pts',(-2.94603200136559,2.549797875,-1.56130090304574E-16));
#10050=CARTESIAN_POINT('Ctrl Pts',(-2.88353200136559,2.549797875,1.0561608611351));
#10051=CARTESIAN_POINT('Ctrl Pts',(-2.82103200136559,1.80297936806755,1.80297936806755));
#10052=CARTESIAN_POINT('Ctrl Pts',(-2.75853200136559,1.0561608611351,2.549797875));
#10053=CARTESIAN_POINT('Ctrl Pts',(-2.6960320013656,3.12260180609148E-16,
2.549797875));
#10054=CARTESIAN_POINT('Ctrl Pts',(-4.50855844600304,0.,-2.00848619417908));
#10055=CARTESIAN_POINT('Ctrl Pts',(-4.44605844600304,0.831942221468096,
-2.00848619417908));
#10056=CARTESIAN_POINT('Ctrl Pts',(-4.38355844600304,1.42021420782359,-1.42021420782359));
#10057=CARTESIAN_POINT('Ctrl Pts',(-4.32105844600304,2.00848619417908,-0.831942221468096));
#10058=CARTESIAN_POINT('Ctrl Pts',(-4.25855844600304,2.00848619417908,-1.22984309441653E-16));
#10059=CARTESIAN_POINT('Ctrl Pts',(-4.19605844600304,2.00848619417908,0.831942221468096));
#10060=CARTESIAN_POINT('Ctrl Pts',(-4.13355844600304,1.42021420782359,1.42021420782359));
#10061=CARTESIAN_POINT('Ctrl Pts',(-4.07105844600304,0.831942221468096,
2.00848619417908));
#10062=CARTESIAN_POINT('Ctrl Pts',(-4.00855844600304,2.45968618883306E-16,
2.00848619417908));
#10063=CARTESIAN_POINT('Ctrl Pts',(-3.94605844600304,-0.831942221468095,
2.00848619417908));
#10064=CARTESIAN_POINT('Ctrl Pts',(-3.88355844600304,-1.42021420782359,
1.42021420782359));
#10065=CARTESIAN_POINT('Ctrl Pts',(-3.82105844600304,-2.00848619417908,
0.831942221468097));
#10066=CARTESIAN_POINT('Ctrl Pts',(-3.75855844600304,-2.00848619417908,
3.68952928324959E-16));
#10067=CARTESIAN_POINT('Ctrl Pts',(-3.69605844600304,-2.00848619417908,
-0.831942221468096));
#10068=CARTESIAN_POINT('Ctrl Pts',(-3.63355844600304,-1.42021420782359,
-1.42021420782359));
#10069=CARTESIAN_POINT('Ctrl Pts',(-3.57105844600304,-0.831942221468097,
-2.00848619417908));
#10070=CARTESIAN_POINT('Ctrl Pts',(-3.50855844600304,0.,-2.00848619417908));
#10071=CARTESIAN_POINT('Ctrl Pts',(-3.44605844600304,0.831942221468096,
-2.00848619417908));
#10072=CARTESIAN_POINT('Ctrl Pts',(-3.38355844600304,1.42021420782359,-1.42021420782359));
#10073=CARTESIAN_POINT('Ctrl Pts',(-3.32105844600304,2.00848619417908,-0.831942221468096));
#10074=CARTESIAN_POINT('Ctrl Pts',(-3.25855844600304,2.00848619417908,-1.22984309441653E-16));
#10075=CARTESIAN_POINT('Ctrl Pts',(-3.19605844600304,2.00848619417908,0.831942221468096));
#10076=CARTESIAN_POINT('Ctrl Pts',(-3.13355844600304,1.42021420782359,1.42021420782359));
#10077=CARTESIAN_POINT('Ctrl Pts',(-3.07105844600304,0.831942221468096,
2.00848619417908));
#10078=CARTESIAN_POINT('Ctrl Pts',(-3.00855844600304,2.45968618883306E-16,
2.00848619417908));
#10079=CARTESIAN_POINT('Ctrl Pts',(-2.94605844600304,-0.831942221468095,
2.00848619417908));
#10080=CARTESIAN_POINT('Ctrl Pts',(-2.88355844600304,-1.42021420782359,
1.42021420782359));
#10081=CARTESIAN_POINT('Ctrl Pts',(-2.82105844600304,-2.00848619417908,
0.831942221468097));
#10082=CARTESIAN_POINT('Ctrl Pts',(-2.75855844600304,-2.00848619417908,
3.68952928324959E-16));
#10083=CARTESIAN_POINT('Ctrl Pts',(-2.69605844600304,-2.00848619417908,
-0.831942221468096));
#10084=CARTESIAN_POINT('Ctrl Pts',(-2.63355844600304,-1.42021420782359,
-1.42021420782359));
#10085=CARTESIAN_POINT('Ctrl Pts',(-2.57105844600304,-0.831942221468097,
-2.00848619417908));
#10086=CARTESIAN_POINT('Ctrl Pts',(-2.50855844600304,0.,-2.00848619417908));
#10087=CARTESIAN_POINT('Ctrl Pts',(-2.44605844600304,0.831942221468096,
-2.00848619417908));
#10088=CARTESIAN_POINT('Ctrl Pts',(-2.38355844600304,1.42021420782359,-1.42021420782359));
#10089=CARTESIAN_POINT('Ctrl Pts',(-2.32105844600304,2.00848619417908,-0.831942221468096));
#10090=CARTESIAN_POINT('Ctrl Pts',(-2.25855844600304,2.00848619417908,-1.22984309441653E-16));
#10091=CARTESIAN_POINT('Ctrl Pts',(-2.19605844600304,2.00848619417908,0.831942221468096));
#10092=CARTESIAN_POINT('Ctrl Pts',(-2.13355844600304,1.42021420782359,1.42021420782359));
#10093=CARTESIAN_POINT('Ctrl Pts',(-2.07105844600304,0.831942221468096,
2.00848619417908));
#10094=CARTESIAN_POINT('Ctrl Pts',(-2.00855844600304,2.45968618883306E-16,
2.00848619417908));
#10095=CARTESIAN_POINT('Ctrl Pts',(-1.94605844600304,-0.831942221468095,
2.00848619417908));
#10096=CARTESIAN_POINT('Ctrl Pts',(-1.88355844600304,-1.42021420782359,
1.42021420782359));
#10097=CARTESIAN_POINT('Ctrl Pts',(-1.82105844600304,-2.00848619417908,
0.831942221468097));
#10098=CARTESIAN_POINT('Ctrl Pts',(-1.75855844600304,-2.00848619417908,
3.68952928324959E-16));
#10099=CARTESIAN_POINT('Ctrl Pts',(-1.69605844600304,-2.00848619417908,
-0.831942221468096));
#10100=CARTESIAN_POINT('Ctrl Pts',(-1.63355844600304,-1.42021420782359,
-1.42021420782359));
#10101=CARTESIAN_POINT('Ctrl Pts',(-1.57105844600304,-0.831942221468097,
-2.00848619417908));
#10102=CARTESIAN_POINT('Ctrl Pts',(-1.50855844600304,0.,-2.00848619417908));
#10103=CARTESIAN_POINT('Ctrl Pts',(-1.44605844600304,0.831942221468096,
-2.00848619417908));
#10104=CARTESIAN_POINT('Ctrl Pts',(-1.38355844600304,1.42021420782359,-1.42021420782359));
#10105=CARTESIAN_POINT('Ctrl Pts',(-1.32105844600304,2.00848619417908,-0.831942221468096));
#10106=CARTESIAN_POINT('Ctrl Pts',(-1.25855844600304,2.00848619417908,-1.22984309441653E-16));
#10107=CARTESIAN_POINT('Ctrl Pts',(-1.19605844600304,2.00848619417908,0.831942221468096));
#10108=CARTESIAN_POINT('Ctrl Pts',(-1.13355844600304,1.42021420782359,1.42021420782359));
#10109=CARTESIAN_POINT('Ctrl Pts',(-1.07105844600304,0.831942221468096,
2.00848619417908));
#10110=CARTESIAN_POINT('Ctrl Pts',(-1.00855844600304,2.45968618883306E-16,
2.00848619417908));
#10111=CARTESIAN_POINT('Ctrl Pts',(-0.94605844600304,-0.831942221468095,
2.00848619417908));
#10112=CARTESIAN_POINT('Ctrl Pts',(-0.88355844600304,-1.42021420782359,
1.42021420782359));
#10113=CARTESIAN_POINT('Ctrl Pts',(-0.82105844600304,-2.00848619417908,
0.831942221468097));
#10114=CARTESIAN_POINT('Ctrl Pts',(-0.75855844600304,-2.00848619417908,
3.68952928324959E-16));
#10115=CARTESIAN_POINT('Ctrl Pts',(-0.696058446003041,-2.00848619417908,
-0.831942221468096));
#10116=CARTESIAN_POINT('Ctrl Pts',(-0.63355844600304,-1.42021420782359,
-1.42021420782359));
#10117=CARTESIAN_POINT('Ctrl Pts',(-0.571058446003041,-0.831942221468097,
-2.00848619417908));
#10118=CARTESIAN_POINT('Ctrl Pts',(-0.50855844600304,0.,-2.00848619417908));
#10119=CARTESIAN_POINT('Ctrl Pts',(-0.446058446003041,0.831942221468096,
-2.00848619417908));
#10120=CARTESIAN_POINT('Ctrl Pts',(-0.38355844600304,1.42021420782359,-1.42021420782359));
#10121=CARTESIAN_POINT('Ctrl Pts',(-0.321058446003041,2.00848619417908,
-0.831942221468096));
#10122=CARTESIAN_POINT('Ctrl Pts',(-0.25855844600304,2.00848619417908,-1.22984309441653E-16));
#10123=CARTESIAN_POINT('Ctrl Pts',(-0.19605844600304,2.00848619417908,0.831942221468096));
#10124=CARTESIAN_POINT('Ctrl Pts',(-0.13355844600304,1.42021420782359,1.42021420782359));
#10125=CARTESIAN_POINT('Ctrl Pts',(-0.0710584460030402,0.831942221468096,
2.00848619417908));
#10126=CARTESIAN_POINT('Ctrl Pts',(-0.00855844600304013,2.45968618883306E-16,
2.00848619417908));
#10127=CARTESIAN_POINT('Ctrl Pts',(0.0539415539969591,-0.831942221468095,
2.00848619417908));
#10128=CARTESIAN_POINT('Ctrl Pts',(0.11644155399696,-1.42021420782359,1.42021420782359));
#10129=CARTESIAN_POINT('Ctrl Pts',(0.178941553996959,-2.00848619417908,
0.831942221468097));
#10130=CARTESIAN_POINT('Ctrl Pts',(0.24144155399696,-2.00848619417908,3.68952928324959E-16));
#10131=CARTESIAN_POINT('Ctrl Pts',(0.303941553996959,-2.00848619417908,
-0.831942221468096));
#10132=CARTESIAN_POINT('Ctrl Pts',(0.36644155399696,-1.42021420782359,-1.42021420782359));
#10133=CARTESIAN_POINT('Ctrl Pts',(0.428941553996959,-0.831942221468097,
-2.00848619417908));
#10134=CARTESIAN_POINT('Ctrl Pts',(0.49144155399696,0.,-2.00848619417908));
#10135=CARTESIAN_POINT('Ctrl Pts',(-4.19603200136559,0.,-2.549797875));
#10136=CARTESIAN_POINT('Ctrl Pts',(-4.13353200136559,1.0561608611351,-2.549797875));
#10137=CARTESIAN_POINT('Ctrl Pts',(-4.07103200136559,1.80297936806755,-1.80297936806755));
#10138=CARTESIAN_POINT('Ctrl Pts',(-4.00853200136559,2.549797875,-1.0561608611351));
#10139=CARTESIAN_POINT('Ctrl Pts',(-3.9460320013656,2.549797875,-1.56130090304574E-16));
#10140=CARTESIAN_POINT('Ctrl Pts',(-3.88353200136559,2.549797875,1.0561608611351));
#10141=CARTESIAN_POINT('Ctrl Pts',(-3.8210320013656,1.80297936806755,1.80297936806755));
#10142=CARTESIAN_POINT('Ctrl Pts',(-3.75853200136559,1.0561608611351,2.549797875));
#10143=CARTESIAN_POINT('Ctrl Pts',(-3.6960320013656,3.12260180609148E-16,
2.549797875));
#10144=CARTESIAN_POINT('Ctrl Pts',(-3.63353200136559,-1.0561608611351,2.549797875));
#10145=CARTESIAN_POINT('Ctrl Pts',(-3.57103200136559,-1.80297936806755,
1.80297936806755));
#10146=CARTESIAN_POINT('Ctrl Pts',(-3.50853200136559,-2.549797875,1.0561608611351));
#10147=CARTESIAN_POINT('Ctrl Pts',(-3.4460320013656,-2.549797875,4.68390270913721E-16));
#10148=CARTESIAN_POINT('Ctrl Pts',(-3.3835320013656,-2.549797875,-1.0561608611351));
#10149=CARTESIAN_POINT('Ctrl Pts',(-3.3210320013656,-1.80297936806755,-1.80297936806755));
#10150=CARTESIAN_POINT('Ctrl Pts',(-3.2585320013656,-1.0561608611351,-2.549797875));
#10151=CARTESIAN_POINT('Ctrl Pts',(-3.1960320013656,0.,-2.549797875));
#10152=CARTESIAN_POINT('Ctrl Pts',(-3.13353200136559,1.0561608611351,-2.549797875));
#10153=CARTESIAN_POINT('Ctrl Pts',(-3.07103200136559,1.80297936806755,-1.80297936806755));
#10154=CARTESIAN_POINT('Ctrl Pts',(-3.00853200136559,2.549797875,-1.0561608611351));
#10155=CARTESIAN_POINT('Ctrl Pts',(-2.94603200136559,2.549797875,-1.56130090304574E-16));
#10156=CARTESIAN_POINT('Ctrl Pts',(-2.88353200136559,2.549797875,1.0561608611351));
#10157=CARTESIAN_POINT('Ctrl Pts',(-2.82103200136559,1.80297936806755,1.80297936806755));
#10158=CARTESIAN_POINT('Ctrl Pts',(-2.75853200136559,1.0561608611351,2.549797875));
#10159=CARTESIAN_POINT('Ctrl Pts',(-2.6960320013656,3.12260180609148E-16,
2.549797875));
#10160=CARTESIAN_POINT('Ctrl Pts',(-2.63353200136559,-1.0561608611351,2.549797875));
#10161=CARTESIAN_POINT('Ctrl Pts',(-2.5710320013656,-1.80297936806755,1.80297936806755));
#10162=CARTESIAN_POINT('Ctrl Pts',(-2.5085320013656,-2.549797875,1.0561608611351));
#10163=CARTESIAN_POINT('Ctrl Pts',(-2.44603200136559,-2.549797875,4.68390270913721E-16));
#10164=CARTESIAN_POINT('Ctrl Pts',(-2.38353200136559,-2.549797875,-1.0561608611351));
#10165=CARTESIAN_POINT('Ctrl Pts',(-2.3210320013656,-1.80297936806755,-1.80297936806755));
#10166=CARTESIAN_POINT('Ctrl Pts',(-2.25853200136559,-1.0561608611351,-2.549797875));
#10167=CARTESIAN_POINT('Ctrl Pts',(-2.1960320013656,0.,-2.549797875));
#10168=CARTESIAN_POINT('Ctrl Pts',(-2.13353200136559,1.0561608611351,-2.549797875));
#10169=CARTESIAN_POINT('Ctrl Pts',(-2.07103200136559,1.80297936806755,-1.80297936806755));
#10170=CARTESIAN_POINT('Ctrl Pts',(-2.00853200136559,2.549797875,-1.0561608611351));
#10171=CARTESIAN_POINT('Ctrl Pts',(-1.9460320013656,2.549797875,-1.56130090304574E-16));
#10172=CARTESIAN_POINT('Ctrl Pts',(-1.8835320013656,2.549797875,1.0561608611351));
#10173=CARTESIAN_POINT('Ctrl Pts',(-1.82103200136559,1.80297936806755,1.80297936806755));
#10174=CARTESIAN_POINT('Ctrl Pts',(-1.7585320013656,1.0561608611351,2.549797875));
#10175=CARTESIAN_POINT('Ctrl Pts',(-1.69603200136559,3.12260180609148E-16,
2.549797875));
#10176=CARTESIAN_POINT('Ctrl Pts',(-1.63353200136559,-1.0561608611351,2.549797875));
#10177=CARTESIAN_POINT('Ctrl Pts',(-1.5710320013656,-1.80297936806755,1.80297936806755));
#10178=CARTESIAN_POINT('Ctrl Pts',(-1.50853200136559,-2.549797875,1.0561608611351));
#10179=CARTESIAN_POINT('Ctrl Pts',(-1.44603200136559,-2.549797875,4.68390270913721E-16));
#10180=CARTESIAN_POINT('Ctrl Pts',(-1.38353200136559,-2.549797875,-1.0561608611351));
#10181=CARTESIAN_POINT('Ctrl Pts',(-1.32103200136559,-1.80297936806755,
-1.80297936806755));
#10182=CARTESIAN_POINT('Ctrl Pts',(-1.25853200136559,-1.0561608611351,-2.549797875));
#10183=CARTESIAN_POINT('Ctrl Pts',(-1.19603200136559,0.,-2.549797875));
#10184=CARTESIAN_POINT('Ctrl Pts',(-1.13353200136559,1.0561608611351,-2.549797875));
#10185=CARTESIAN_POINT('Ctrl Pts',(-1.07103200136559,1.80297936806755,-1.80297936806755));
#10186=CARTESIAN_POINT('Ctrl Pts',(-1.00853200136559,2.549797875,-1.0561608611351));
#10187=CARTESIAN_POINT('Ctrl Pts',(-0.946032001365594,2.549797875,-1.56130090304574E-16));
#10188=CARTESIAN_POINT('Ctrl Pts',(-0.883532001365594,2.549797875,1.0561608611351));
#10189=CARTESIAN_POINT('Ctrl Pts',(-0.821032001365594,1.80297936806755,
1.80297936806755));
#10190=CARTESIAN_POINT('Ctrl Pts',(-0.758532001365594,1.0561608611351,2.549797875));
#10191=CARTESIAN_POINT('Ctrl Pts',(-0.696032001365594,3.12260180609148E-16,
2.549797875));
#10192=CARTESIAN_POINT('Ctrl Pts',(-0.633532001365594,-1.0561608611351,
2.549797875));
#10193=CARTESIAN_POINT('Ctrl Pts',(-0.571032001365594,-1.80297936806755,
1.80297936806755));
#10194=CARTESIAN_POINT('Ctrl Pts',(-0.508532001365594,-2.549797875,1.0561608611351));
#10195=CARTESIAN_POINT('Ctrl Pts',(-0.446032001365594,-2.549797875,4.68390270913721E-16));
#10196=CARTESIAN_POINT('Ctrl Pts',(-0.383532001365594,-2.549797875,-1.0561608611351));
#10197=CARTESIAN_POINT('Ctrl Pts',(-0.321032001365594,-1.80297936806755,
-1.80297936806755));
#10198=CARTESIAN_POINT('Ctrl Pts',(-0.258532001365594,-1.0561608611351,
-2.549797875));
#10199=CARTESIAN_POINT('Ctrl Pts',(-0.196032001365594,0.,-2.549797875));
#10200=CARTESIAN_POINT('Ctrl Pts',(-0.133532001365594,1.0561608611351,-2.549797875));
#10201=CARTESIAN_POINT('Ctrl Pts',(-0.0710320013655938,1.80297936806755,
-1.80297936806755));
#10202=CARTESIAN_POINT('Ctrl Pts',(-0.00853200136559373,2.549797875,-1.0561608611351));
#10203=CARTESIAN_POINT('Ctrl Pts',(0.0539679986344063,2.549797875,-1.56130090304574E-16));
#10204=CARTESIAN_POINT('Ctrl Pts',(0.116467998634406,2.549797875,1.0561608611351));
#10205=CARTESIAN_POINT('Ctrl Pts',(0.178967998634407,1.80297936806755,1.80297936806755));
#10206=CARTESIAN_POINT('Ctrl Pts',(0.241467998634406,1.0561608611351,2.549797875));
#10207=CARTESIAN_POINT('Ctrl Pts',(0.303967998634406,3.12260180609148E-16,
2.549797875));
#10208=CARTESIAN_POINT('Ctrl Pts',(0.366467998634406,-1.0561608611351,2.549797875));
#10209=CARTESIAN_POINT('Ctrl Pts',(0.428967998634406,-1.80297936806755,
1.80297936806755));
#10210=CARTESIAN_POINT('Ctrl Pts',(0.491467998634406,-2.549797875,1.0561608611351));
#10211=CARTESIAN_POINT('Ctrl Pts',(0.553967998634406,-2.549797875,4.68390270913721E-16));
#10212=CARTESIAN_POINT('Ctrl Pts',(0.616467998634407,-2.549797875,-1.0561608611351));
#10213=CARTESIAN_POINT('Ctrl Pts',(0.678967998634406,-1.80297936806755,
-1.80297936806755));
#10214=CARTESIAN_POINT('Ctrl Pts',(0.741467998634407,-1.0561608611351,-2.549797875));
#10215=CARTESIAN_POINT('Ctrl Pts',(0.803967998634406,0.,-2.549797875));
#10216=CARTESIAN_POINT('Ctrl Pts',(-4.07103200136559,0.,-2.549797875));
#10217=CARTESIAN_POINT('Ctrl Pts',(-4.00853200136559,1.0561608611351,-2.549797875));
#10218=CARTESIAN_POINT('Ctrl Pts',(-3.9460320013656,1.80297936806755,-1.80297936806755));
#10219=CARTESIAN_POINT('Ctrl Pts',(-3.88353200136559,2.549797875,-1.0561608611351));
#10220=CARTESIAN_POINT('Ctrl Pts',(-3.8210320013656,2.549797875,-1.56130090304574E-16));
#10221=CARTESIAN_POINT('Ctrl Pts',(-3.75853200136559,2.549797875,1.0561608611351));
#10222=CARTESIAN_POINT('Ctrl Pts',(-3.6960320013656,1.80297936806755,1.80297936806755));
#10223=CARTESIAN_POINT('Ctrl Pts',(-3.63353200136559,1.0561608611351,2.549797875));
#10224=CARTESIAN_POINT('Ctrl Pts',(-3.57103200136559,3.12260180609148E-16,
2.549797875));
#10225=CARTESIAN_POINT('Ctrl Pts',(-3.50853200136559,-1.0561608611351,2.549797875));
#10226=CARTESIAN_POINT('Ctrl Pts',(-3.4460320013656,-1.80297936806755,1.80297936806755));
#10227=CARTESIAN_POINT('Ctrl Pts',(-3.3835320013656,-2.549797875,1.0561608611351));
#10228=CARTESIAN_POINT('Ctrl Pts',(-3.3210320013656,-2.549797875,4.68390270913721E-16));
#10229=CARTESIAN_POINT('Ctrl Pts',(-3.2585320013656,-2.549797875,-1.0561608611351));
#10230=CARTESIAN_POINT('Ctrl Pts',(-3.1960320013656,-1.80297936806755,-1.80297936806755));
#10231=CARTESIAN_POINT('Ctrl Pts',(-3.13353200136559,-1.0561608611351,-2.549797875));
#10232=CARTESIAN_POINT('Ctrl Pts',(-3.07103200136559,0.,-2.549797875));
#10233=CARTESIAN_POINT('Ctrl Pts',(-3.00853200136559,1.0561608611351,-2.549797875));
#10234=CARTESIAN_POINT('Ctrl Pts',(-2.94603200136559,1.80297936806755,-1.80297936806755));
#10235=CARTESIAN_POINT('Ctrl Pts',(-2.88353200136559,2.549797875,-1.0561608611351));
#10236=CARTESIAN_POINT('Ctrl Pts',(-2.82103200136559,2.549797875,-1.56130090304574E-16));
#10237=CARTESIAN_POINT('Ctrl Pts',(-2.75853200136559,2.549797875,1.0561608611351));
#10238=CARTESIAN_POINT('Ctrl Pts',(-2.6960320013656,1.80297936806755,1.80297936806755));
#10239=CARTESIAN_POINT('Ctrl Pts',(-2.63353200136559,1.0561608611351,2.549797875));
#10240=CARTESIAN_POINT('Ctrl Pts',(-2.5710320013656,3.12260180609148E-16,
2.549797875));
#10241=CARTESIAN_POINT('Ctrl Pts',(-2.5085320013656,-1.0561608611351,2.549797875));
#10242=CARTESIAN_POINT('Ctrl Pts',(-2.44603200136559,-1.80297936806755,
1.80297936806755));
#10243=CARTESIAN_POINT('Ctrl Pts',(-2.38353200136559,-2.549797875,1.0561608611351));
#10244=CARTESIAN_POINT('Ctrl Pts',(-2.3210320013656,-2.549797875,4.68390270913721E-16));
#10245=CARTESIAN_POINT('Ctrl Pts',(-2.25853200136559,-2.549797875,-1.0561608611351));
#10246=CARTESIAN_POINT('Ctrl Pts',(-2.1960320013656,-1.80297936806755,-1.80297936806755));
#10247=CARTESIAN_POINT('Ctrl Pts',(-2.13353200136559,-1.0561608611351,-2.549797875));
#10248=CARTESIAN_POINT('Ctrl Pts',(-2.07103200136559,0.,-2.549797875));
#10249=CARTESIAN_POINT('Ctrl Pts',(-2.00853200136559,1.0561608611351,-2.549797875));
#10250=CARTESIAN_POINT('Ctrl Pts',(-1.9460320013656,1.80297936806755,-1.80297936806755));
#10251=CARTESIAN_POINT('Ctrl Pts',(-1.8835320013656,2.549797875,-1.0561608611351));
#10252=CARTESIAN_POINT('Ctrl Pts',(-1.82103200136559,2.549797875,-1.56130090304574E-16));
#10253=CARTESIAN_POINT('Ctrl Pts',(-1.7585320013656,2.549797875,1.0561608611351));
#10254=CARTESIAN_POINT('Ctrl Pts',(-1.69603200136559,1.80297936806755,1.80297936806755));
#10255=CARTESIAN_POINT('Ctrl Pts',(-1.63353200136559,1.0561608611351,2.549797875));
#10256=CARTESIAN_POINT('Ctrl Pts',(-1.5710320013656,3.12260180609148E-16,
2.549797875));
#10257=CARTESIAN_POINT('Ctrl Pts',(-1.50853200136559,-1.0561608611351,2.549797875));
#10258=CARTESIAN_POINT('Ctrl Pts',(-1.44603200136559,-1.80297936806755,
1.80297936806755));
#10259=CARTESIAN_POINT('Ctrl Pts',(-1.38353200136559,-2.549797875,1.0561608611351));
#10260=CARTESIAN_POINT('Ctrl Pts',(-1.32103200136559,-2.549797875,4.68390270913721E-16));
#10261=CARTESIAN_POINT('Ctrl Pts',(-1.25853200136559,-2.549797875,-1.0561608611351));
#10262=CARTESIAN_POINT('Ctrl Pts',(-1.19603200136559,-1.80297936806755,
-1.80297936806755));
#10263=CARTESIAN_POINT('Ctrl Pts',(-1.13353200136559,-1.0561608611351,-2.549797875));
#10264=CARTESIAN_POINT('Ctrl Pts',(-1.07103200136559,0.,-2.549797875));
#10265=CARTESIAN_POINT('Ctrl Pts',(-1.00853200136559,1.0561608611351,-2.549797875));
#10266=CARTESIAN_POINT('Ctrl Pts',(-0.946032001365594,1.80297936806755,
-1.80297936806755));
#10267=CARTESIAN_POINT('Ctrl Pts',(-0.883532001365593,2.549797875,-1.0561608611351));
#10268=CARTESIAN_POINT('Ctrl Pts',(-0.821032001365594,2.549797875,-1.56130090304574E-16));
#10269=CARTESIAN_POINT('Ctrl Pts',(-0.758532001365594,2.549797875,1.0561608611351));
#10270=CARTESIAN_POINT('Ctrl Pts',(-0.696032001365594,1.80297936806755,
1.80297936806755));
#10271=CARTESIAN_POINT('Ctrl Pts',(-0.633532001365594,1.0561608611351,2.549797875));
#10272=CARTESIAN_POINT('Ctrl Pts',(-0.571032001365594,3.12260180609148E-16,
2.549797875));
#10273=CARTESIAN_POINT('Ctrl Pts',(-0.508532001365594,-1.0561608611351,
2.549797875));
#10274=CARTESIAN_POINT('Ctrl Pts',(-0.446032001365594,-1.80297936806755,
1.80297936806755));
#10275=CARTESIAN_POINT('Ctrl Pts',(-0.383532001365594,-2.549797875,1.0561608611351));
#10276=CARTESIAN_POINT('Ctrl Pts',(-0.321032001365594,-2.549797875,4.68390270913721E-16));
#10277=CARTESIAN_POINT('Ctrl Pts',(-0.258532001365594,-2.549797875,-1.0561608611351));
#10278=CARTESIAN_POINT('Ctrl Pts',(-0.196032001365594,-1.80297936806755,
-1.80297936806755));
#10279=CARTESIAN_POINT('Ctrl Pts',(-0.133532001365594,-1.0561608611351,
-2.549797875));
#10280=CARTESIAN_POINT('Ctrl Pts',(-0.0710320013655938,0.,-2.549797875));
#10281=CARTESIAN_POINT('Ctrl Pts',(-0.00853200136559373,1.0561608611351,
-2.549797875));
#10282=CARTESIAN_POINT('Ctrl Pts',(0.0539679986344063,1.80297936806755,
-1.80297936806755));
#10283=CARTESIAN_POINT('Ctrl Pts',(0.116467998634406,2.549797875,-1.0561608611351));
#10284=CARTESIAN_POINT('Ctrl Pts',(0.178967998634407,2.549797875,-1.56130090304574E-16));
#10285=CARTESIAN_POINT('Ctrl Pts',(0.241467998634406,2.549797875,1.0561608611351));
#10286=CARTESIAN_POINT('Ctrl Pts',(0.303967998634406,1.80297936806755,1.80297936806755));
#10287=CARTESIAN_POINT('Ctrl Pts',(0.366467998634407,1.0561608611351,2.549797875));
#10288=CARTESIAN_POINT('Ctrl Pts',(0.428967998634406,3.12260180609148E-16,
2.549797875));
#10289=CARTESIAN_POINT('Ctrl Pts',(0.491467998634406,-1.0561608611351,2.549797875));
#10290=CARTESIAN_POINT('Ctrl Pts',(0.553967998634406,-1.80297936806755,
1.80297936806755));
#10291=CARTESIAN_POINT('Ctrl Pts',(0.616467998634407,-2.549797875,1.0561608611351));
#10292=CARTESIAN_POINT('Ctrl Pts',(0.678967998634406,-2.549797875,4.68390270913721E-16));
#10293=CARTESIAN_POINT('Ctrl Pts',(0.741467998634407,-2.549797875,-1.0561608611351));
#10294=CARTESIAN_POINT('Ctrl Pts',(0.803967998634406,-1.80297936806755,
-1.80297936806755));
#10295=CARTESIAN_POINT('Ctrl Pts',(0.866467998634405,-1.0561608611351,-2.549797875));
#10296=CARTESIAN_POINT('Ctrl Pts',(0.928967998634406,0.,-2.549797875));
#10297=CARTESIAN_POINT('Ctrl Pts',(-3.75852561669427,0.,-2.00852093905959));
#10298=CARTESIAN_POINT('Ctrl Pts',(-3.69602561669426,0.831956613268825,
-2.00852093905959));
#10299=CARTESIAN_POINT('Ctrl Pts',(-3.63352561669426,1.42023877616421,-1.42023877616421));
#10300=CARTESIAN_POINT('Ctrl Pts',(-3.57102561669426,2.00852093905959,-0.831956613268825));
#10301=CARTESIAN_POINT('Ctrl Pts',(-3.50852561669426,2.00852093905959,-1.22986436951988E-16));
#10302=CARTESIAN_POINT('Ctrl Pts',(-3.44602561669426,2.00852093905959,0.831956613268825));
#10303=CARTESIAN_POINT('Ctrl Pts',(-3.38352561669426,1.42023877616421,1.42023877616421));
#10304=CARTESIAN_POINT('Ctrl Pts',(-3.32102561669426,0.831956613268825,
2.00852093905959));
#10305=CARTESIAN_POINT('Ctrl Pts',(-3.25852561669427,2.45972873903976E-16,
2.00852093905959));
#10306=CARTESIAN_POINT('Ctrl Pts',(-3.19602561669426,-0.831956613268824,
2.00852093905959));
#10307=CARTESIAN_POINT('Ctrl Pts',(-3.13352561669426,-1.42023877616421,
1.42023877616421));
#10308=CARTESIAN_POINT('Ctrl Pts',(-3.07102561669426,-2.00852093905959,
0.831956613268827));
#10309=CARTESIAN_POINT('Ctrl Pts',(-3.00852561669426,-2.00852093905959,
3.68959310855964E-16));
#10310=CARTESIAN_POINT('Ctrl Pts',(-2.94602561669426,-2.00852093905959,
-0.831956613268825));
#10311=CARTESIAN_POINT('Ctrl Pts',(-2.88352561669426,-1.42023877616421,
-1.42023877616421));
#10312=CARTESIAN_POINT('Ctrl Pts',(-2.82102561669426,-0.831956613268827,
-2.00852093905959));
#10313=CARTESIAN_POINT('Ctrl Pts',(-2.75852561669427,0.,-2.00852093905959));
#10314=CARTESIAN_POINT('Ctrl Pts',(-2.69602561669426,0.831956613268825,
-2.00852093905959));
#10315=CARTESIAN_POINT('Ctrl Pts',(-2.63352561669426,1.42023877616421,-1.42023877616421));
#10316=CARTESIAN_POINT('Ctrl Pts',(-2.57102561669426,2.00852093905959,-0.831956613268825));
#10317=CARTESIAN_POINT('Ctrl Pts',(-2.50852561669426,2.00852093905959,-1.22986436951988E-16));
#10318=CARTESIAN_POINT('Ctrl Pts',(-2.44602561669426,2.00852093905959,0.831956613268825));
#10319=CARTESIAN_POINT('Ctrl Pts',(-2.38352561669426,1.42023877616421,1.42023877616421));
#10320=CARTESIAN_POINT('Ctrl Pts',(-2.32102561669426,0.831956613268825,
2.00852093905959));
#10321=CARTESIAN_POINT('Ctrl Pts',(-2.25852561669426,2.45972873903976E-16,
2.00852093905959));
#10322=CARTESIAN_POINT('Ctrl Pts',(-2.19602561669426,-0.831956613268824,
2.00852093905959));
#10323=CARTESIAN_POINT('Ctrl Pts',(-2.13352561669426,-1.42023877616421,
1.42023877616421));
#10324=CARTESIAN_POINT('Ctrl Pts',(-2.07102561669426,-2.00852093905959,
0.831956613268827));
#10325=CARTESIAN_POINT('Ctrl Pts',(-2.00852561669426,-2.00852093905959,
3.68959310855964E-16));
#10326=CARTESIAN_POINT('Ctrl Pts',(-1.94602561669426,-2.00852093905959,
-0.831956613268825));
#10327=CARTESIAN_POINT('Ctrl Pts',(-1.88352561669426,-1.42023877616421,
-1.42023877616421));
#10328=CARTESIAN_POINT('Ctrl Pts',(-1.82102561669426,-0.831956613268827,
-2.00852093905959));
#10329=CARTESIAN_POINT('Ctrl Pts',(-1.75852561669426,0.,-2.00852093905959));
#10330=CARTESIAN_POINT('Ctrl Pts',(-1.69602561669426,0.831956613268825,
-2.00852093905959));
#10331=CARTESIAN_POINT('Ctrl Pts',(-1.63352561669426,1.42023877616421,-1.42023877616421));
#10332=CARTESIAN_POINT('Ctrl Pts',(-1.57102561669426,2.00852093905959,-0.831956613268825));
#10333=CARTESIAN_POINT('Ctrl Pts',(-1.50852561669426,2.00852093905959,-1.22986436951988E-16));
#10334=CARTESIAN_POINT('Ctrl Pts',(-1.44602561669426,2.00852093905959,0.831956613268825));
#10335=CARTESIAN_POINT('Ctrl Pts',(-1.38352561669426,1.42023877616421,1.42023877616421));
#10336=CARTESIAN_POINT('Ctrl Pts',(-1.32102561669426,0.831956613268825,
2.00852093905959));
#10337=CARTESIAN_POINT('Ctrl Pts',(-1.25852561669426,2.45972873903976E-16,
2.00852093905959));
#10338=CARTESIAN_POINT('Ctrl Pts',(-1.19602561669426,-0.831956613268824,
2.00852093905959));
#10339=CARTESIAN_POINT('Ctrl Pts',(-1.13352561669426,-1.42023877616421,
1.42023877616421));
#10340=CARTESIAN_POINT('Ctrl Pts',(-1.07102561669426,-2.00852093905959,
0.831956613268827));
#10341=CARTESIAN_POINT('Ctrl Pts',(-1.00852561669426,-2.00852093905959,
3.68959310855964E-16));
#10342=CARTESIAN_POINT('Ctrl Pts',(-0.946025616694262,-2.00852093905959,
-0.831956613268825));
#10343=CARTESIAN_POINT('Ctrl Pts',(-0.883525616694262,-1.42023877616421,
-1.42023877616421));
#10344=CARTESIAN_POINT('Ctrl Pts',(-0.821025616694261,-0.831956613268827,
-2.00852093905959));
#10345=CARTESIAN_POINT('Ctrl Pts',(-0.758525616694262,0.,-2.00852093905959));
#10346=CARTESIAN_POINT('Ctrl Pts',(-0.696025616694261,0.831956613268825,
-2.00852093905959));
#10347=CARTESIAN_POINT('Ctrl Pts',(-0.633525616694262,1.42023877616421,
-1.42023877616421));
#10348=CARTESIAN_POINT('Ctrl Pts',(-0.571025616694261,2.00852093905959,
-0.831956613268825));
#10349=CARTESIAN_POINT('Ctrl Pts',(-0.508525616694262,2.00852093905959,
-1.22986436951988E-16));
#10350=CARTESIAN_POINT('Ctrl Pts',(-0.446025616694262,2.00852093905959,
0.831956613268825));
#10351=CARTESIAN_POINT('Ctrl Pts',(-0.383525616694262,1.42023877616421,
1.42023877616421));
#10352=CARTESIAN_POINT('Ctrl Pts',(-0.321025616694262,0.831956613268825,
2.00852093905959));
#10353=CARTESIAN_POINT('Ctrl Pts',(-0.258525616694262,2.45972873903976E-16,
2.00852093905959));
#10354=CARTESIAN_POINT('Ctrl Pts',(-0.196025616694262,-0.831956613268824,
2.00852093905959));
#10355=CARTESIAN_POINT('Ctrl Pts',(-0.133525616694262,-1.42023877616421,
1.42023877616421));
#10356=CARTESIAN_POINT('Ctrl Pts',(-0.0710256166942618,-2.00852093905959,
0.831956613268827));
#10357=CARTESIAN_POINT('Ctrl Pts',(-0.00852561669426215,-2.00852093905959,
3.68959310855964E-16));
#10358=CARTESIAN_POINT('Ctrl Pts',(0.0539743833057379,-2.00852093905959,
-0.831956613268825));
#10359=CARTESIAN_POINT('Ctrl Pts',(0.116474383305738,-1.42023877616421,
-1.42023877616421));
#10360=CARTESIAN_POINT('Ctrl Pts',(0.178974383305738,-0.831956613268827,
-2.00852093905959));
#10361=CARTESIAN_POINT('Ctrl Pts',(0.241474383305738,0.,-2.00852093905959));
#10362=CARTESIAN_POINT('Ctrl Pts',(0.303974383305738,0.831956613268825,
-2.00852093905959));
#10363=CARTESIAN_POINT('Ctrl Pts',(0.366474383305738,1.42023877616421,-1.42023877616421));
#10364=CARTESIAN_POINT('Ctrl Pts',(0.428974383305738,2.00852093905959,-0.831956613268825));
#10365=CARTESIAN_POINT('Ctrl Pts',(0.491474383305738,2.00852093905959,-1.22986436951988E-16));
#10366=CARTESIAN_POINT('Ctrl Pts',(0.553974383305738,2.00852093905959,0.831956613268825));
#10367=CARTESIAN_POINT('Ctrl Pts',(0.616474383305739,1.42023877616421,1.42023877616421));
#10368=CARTESIAN_POINT('Ctrl Pts',(0.678974383305738,0.831956613268825,
2.00852093905959));
#10369=CARTESIAN_POINT('Ctrl Pts',(0.741474383305739,2.45972873903976E-16,
2.00852093905959));
#10370=CARTESIAN_POINT('Ctrl Pts',(0.803974383305737,-0.831956613268824,
2.00852093905959));
#10371=CARTESIAN_POINT('Ctrl Pts',(0.866474383305738,-1.42023877616421,
1.42023877616421));
#10372=CARTESIAN_POINT('Ctrl Pts',(0.928974383305737,-2.00852093905959,
0.831956613268827));
#10373=CARTESIAN_POINT('Ctrl Pts',(0.991474383305738,-2.00852093905959,
3.68959310855964E-16));
#10374=CARTESIAN_POINT('Ctrl Pts',(1.05397438330574,-2.00852093905959,-0.831956613268825));
#10375=CARTESIAN_POINT('Ctrl Pts',(1.11647438330574,-1.42023877616421,-1.42023877616421));
#10376=CARTESIAN_POINT('Ctrl Pts',(1.17897438330574,-0.831956613268827,
-2.00852093905959));
#10377=CARTESIAN_POINT('Ctrl Pts',(1.24147438330574,0.,-2.00852093905959));
#10402=UNCERTAINTY_MEASURE_WITH_UNIT(LENGTH_MEASURE(0.01),#10414,
'DISTANCE_ACCURACY_VALUE',
'Maximum model space distance between geometric entities at asserted c
onnectivities');
#10403=UNCERTAINTY_MEASURE_WITH_UNIT(LENGTH_MEASURE(0.01),#10414,
'DISTANCE_ACCURACY_VALUE',
'Maximum model space distance between geometric entities at asserted c
onnectivities');
#10412=(
GEOMETRIC_REPRESENTATION_CONTEXT(3)
GLOBAL_UNCERTAINTY_ASSIGNED_CONTEXT((#10402))
GLOBAL_UNIT_ASSIGNED_CONTEXT((#10414,#10416,#10417))
REPRESENTATION_CONTEXT('','3D')
);
#10413=(
GEOMETRIC_REPRESENTATION_CONTEXT(3)
GLOBAL_UNCERTAINTY_ASSIGNED_CONTEXT((#10403))
GLOBAL_UNIT_ASSIGNED_CONTEXT((#10414,#10416,#10417))
REPRESENTATION_CONTEXT('','3D')
);
#10414=(
LENGTH_UNIT()
NAMED_UNIT(*)
SI_UNIT(.MILLI.,.METRE.)
);
#10416=(
NAMED_UNIT(*)
PLANE_ANGLE_UNIT()
SI_UNIT($,.RADIAN.)
);
#10417=(
NAMED_UNIT(*)
SI_UNIT($,.STERADIAN.)
SOLID_ANGLE_UNIT()
);
#10426=SHAPE_DEFINITION_REPRESENTATION(#10435,#10460);
#10435=PRODUCT_DEFINITION_SHAPE('',$,#10470);
#10460=SHAPE_REPRESENTATION('',(#6098),#10412);
#10461=PRODUCT_DEFINITION_CONTEXT('part definition',#10490,'design');
#10470=PRODUCT_DEFINITION('Hex Nut M5','Hex Nut M5',#10479,#10461);
#10479=PRODUCT_DEFINITION_FORMATION('',$,#10500);
#10490=APPLICATION_CONTEXT(
'Core Data for Automotive Mechanical Design Process');
#10491=PRODUCT_CONTEXT('part definition',#10490,'mechanical');
#10500=PRODUCT('Hex Nut M5','Hex Nut M5',$,(#10491));
#10503=PRESENTATION_STYLE_ASSIGNMENT((#10507));
#10507=SURFACE_STYLE_USAGE(.BOTH.,#10511);
#10511=SURFACE_SIDE_STYLE('',(#10515));
#10515=SURFACE_STYLE_FILL_AREA(#10519);
#10519=FILL_AREA_STYLE('Opaque(97,158,199)',(#10523));
#10523=FILL_AREA_STYLE_COLOUR('Opaque(97,158,199)',#10527);
#10527=COLOUR_RGB('Opaque(97,158,199)',0.380392156862745,0.619607843137255,
0.780392156862745);
ENDSEC;
END-ISO-10303-21;
